ISO-10303-21;
HEADER;
FILE_DESCRIPTION (('STEP AP214'),
    '1' );
FILE_NAME ('hex flange nut gradea_iso_ISO - 4161 - M5 - N.step',
    '2026-10-31T03:44:21',
    ( '' ),
    ( '' ),
    'SwSTEP 2.0',
    'SolidWorks 2026',
    '' );
FILE_SCHEMA (( 'AUTOMOTIVE_DESIGN' ));
ENDSEC;

DATA;
#46=CARTESIAN_POINT ( 'NONE',  ( 2.000000000000005329, -3.464101615137751722, 0.000000000000000000 ) ) ;
#52=CARTESIAN_POINT ( 'NONE',  ( -2.000000000000006661, 3.464101615137750834, 0.000000000000000000 ) ) ;
#65=ORIENTED_EDGE ( 'NONE', *, *, #19121, .F. ) ;
#71=VERTEX_POINT ( 'NONE', #1398 ) ;
#81=FACE_OUTER_BOUND ( 'NONE', #5769, .T. ) ;
#83=CARTESIAN_POINT ( 'NONE',  ( 4.000000000000000000, -2.309401076758516691, -0.4999999999999995559 ) ) ;
#93=DIRECTION ( 'NONE',  ( 0.000000000000000000, 0.000000000000000000, -1.000000000000000000 ) ) ;
#124=CARTESIAN_POINT ( 'NONE',  ( 1.411581201560190495E-15, 4.862606272033091592, -3.745885042887436622 ) ) ;
#147=B_SPLINE_CURVE_WITH_KNOTS ( 'NONE', 3,
 ( #14538, #3778, #12976, #8661, #17507, #4068 ),
 .UNSPECIFIED., .F., .F.,
 ( 4, 2, 4 ),
 ( 0.000000000000000000, 0.0002095117440854730670, 0.0004190234881709461339 ),
 .UNSPECIFIED. ) ;
#162=VERTEX_POINT ( 'NONE', #1595 ) ;
#204=CARTESIAN_POINT ( 'NONE',  ( -4.204015924366189871, 1.626724848190922446, -3.610627190413390419 ) ) ;
#287=DIRECTION ( 'NONE',  ( -0.000000000000000000, 0.000000000000000000, -1.000000000000000000 ) ) ;
#319=DIRECTION ( 'NONE',  ( 0.8191520442889902442, 1.003171929053522651E-16, -0.5735764363510482688 ) ) ;
#325=AXIS2_PLACEMENT_3D ( 'NONE', #12478, #15527, #6324 ) ;
#336=DIRECTION ( 'NONE',  ( -0.8660254037844373753, 0.5000000000000021094, 0.000000000000000000 ) ) ;
#352=ORIENTED_EDGE ( 'NONE', *, *, #9202, .F. ) ;
#362=ORIENTED_EDGE ( 'NONE', *, *, #7302, .F. ) ;
#363=CARTESIAN_POINT ( 'NONE',  ( -2.000000000000006661, 3.464101615137750834, 0.000000000000000000 ) ) ;
#377=ORIENTED_EDGE ( 'NONE', *, *, #16114, .F. ) ;
#389=CARTESIAN_POINT ( 'NONE',  ( 1.828356344711641102, 3.563200125723180900, -5.433716356636336675E-16 ) ) ;
#410=ADVANCED_FACE ( 'NONE', ( #9796 ), #12997, .T. ) ;
#442=VERTEX_POINT ( 'NONE', #8621 ) ;
#453=DIRECTION ( 'NONE',  ( -1.000000000000000000, 0.000000000000000000, 0.000000000000000000 ) ) ;
#495=CARTESIAN_POINT ( 'NONE',  ( 0.000000000000000000, 0.000000000000000000, -0.2800830152838844622 ) ) ;
#499=CARTESIAN_POINT ( 'NONE',  ( -1.391697335622809950, -4.043246145443391448, -3.503898532754372575 ) ) ;
#509=CARTESIAN_POINT ( 'NONE',  ( 4.197393957002303999, 7.772902908466098641E-14, -3.503767560748929810 ) ) ;
#512=ADVANCED_FACE ( 'NONE', ( #11928, #81 ), #6058, .F. ) ;
#517=DIRECTION ( 'NONE',  ( -0.5000000000000019984, -0.8660254037844375974, 0.000000000000000000 ) ) ;
#522=ADVANCED_FACE ( 'NONE', ( #10646 ), #7666, .F. ) ;
#551=AXIS2_PLACEMENT_3D ( 'NONE', #15450, #17327, #3884 ) ;
#558=ORIENTED_EDGE ( 'NONE', *, *, #7471, .T. ) ;
#560=AXIS2_PLACEMENT_3D ( 'NONE', #12362, #8144, #6676 ) ;
#566=ORIENTED_EDGE ( 'NONE', *, *, #5091, .F. ) ;
#568=ORIENTED_EDGE ( 'NONE', *, *, #6489, .F. ) ;
#592=DIRECTION ( 'NONE',  ( -1.000000000000000000, 0.000000000000000000, 0.000000000000000000 ) ) ;
#643=FACE_OUTER_BOUND ( 'NONE', #735, .T. ) ;
#696=VECTOR ( 'NONE', #16652, 1000.000000000000000 ) ;
#715=EDGE_LOOP ( 'NONE', ( #8908, #4460, #558, #11992 ) ) ;
#735=EDGE_LOOP ( 'NONE', ( #6903, #13575, #566 ) ) ;
#746=CARTESIAN_POINT ( 'NONE',  ( -4.000000000000000000, -2.309401076758512694, -3.433295621305382461 ) ) ;
#749=ORIENTED_EDGE ( 'NONE', *, *, #15883, .T. ) ;
#795=CARTESIAN_POINT ( 'NONE',  ( -2.100000000000000089, 2.571758278209441957E-16, -0.2800830152838844622 ) ) ;
#797=DIRECTION ( 'NONE',  ( 0.000000000000000000, -0.000000000000000000, 1.000000000000000000 ) ) ;
#808=( GEOMETRIC_REPRESENTATION_CONTEXT ( 3 ) GLOBAL_UNCERTAINTY_ASSIGNED_CONTEXT ( ( #5003 ) ) GLOBAL_UNIT_ASSIGNED_CONTEXT ( ( #1553, #2931, #11933 ) ) REPRESENTATION_CONTEXT ( 'NONE', 'WORKASPACE' ) );
#840=DIRECTION ( 'NONE',  ( 0.5000000000000013323, -0.8660254037844379305, 0.000000000000000000 ) ) ;
#848=VERTEX_POINT ( 'NONE', #18900 ) ;
#894=CARTESIAN_POINT ( 'NONE',  ( -2.499999999999999556, 3.061616997868382648E-16, 3.469446951953614189E-15 ) ) ;
#906=CARTESIAN_POINT ( 'NONE',  ( 4.211140560182196957, -2.431303136016555122, -3.745885042887436622 ) ) ;
#907=ORIENTED_EDGE ( 'NONE', *, *, #11164, .T. ) ;
#938=CARTESIAN_POINT ( 'NONE',  ( 2.171643655288379993, -3.365003104552334978, -1.195831703456429434E-14 ) ) ;
#952=EDGE_LOOP ( 'NONE', ( #16267, #2936 ) ) ;
#973=AXIS2_PLACEMENT_3D ( 'NONE', #7810, #1839, #2128 ) ;
#986=ORIENTED_EDGE ( 'NONE', *, *, #18591, .F. ) ;
#996=CARTESIAN_POINT ( 'NONE',  ( 0.000000000000000000, 0.000000000000000000, -5.000000000000000888 ) ) ;
#1008=DIRECTION ( 'NONE',  ( 0.8191520442889875797, 0.000000000000000000, 0.5735764363510522656 ) ) ;
#1014=VERTEX_POINT ( 'NONE', #52 ) ;
#1017=CARTESIAN_POINT ( 'NONE',  ( 1.390230914382191596, 4.043987460488659202, -3.502507215260488582 ) ) ;
#1021=CARTESIAN_POINT ( 'NONE',  ( -4.024497503033519941, 2.323544716729375459, -3.572167766733379768 ) ) ;
#1034=DIRECTION ( 'NONE',  ( 0.000000000000000000, 0.000000000000000000, -1.000000000000000000 ) ) ;
#1041=CARTESIAN_POINT ( 'NONE',  ( 2.000000000000005329, -3.464101615137751722, 0.000000000000000000 ) ) ;
#1098=CARTESIAN_POINT ( 'NONE',  ( -3.472371940586054251, -2.614027278893156669, -3.320322319202162031 ) ) ;
#1128=CARTESIAN_POINT ( 'NONE',  ( 2.855764796983346177, -2.970025579236428737, -0.09382832055446485575 ) ) ;
#1142=B_SPLINE_CURVE_WITH_KNOTS ( 'NONE', 3,
 ( #10723, #1634, #9163, #12196, #15234, #6499, #1815, #10624 ),
 .UNSPECIFIED., .F., .F.,
 ( 4, 2, 2, 4 ),
 ( 0.000000000000000000, 0.002450665683189819262, 0.003675998524784728893, 0.004901331366379639391 ),
 .UNSPECIFIED. ) ;
#1145=ORIENTED_EDGE ( 'NONE', *, *, #1242, .T. ) ;
#1169=CIRCLE ( 'NONE', #13978, 5.384454397937118664 ) ;
#1178=ORIENTED_EDGE ( 'NONE', *, *, #4265, .F. ) ;
#1181=DIRECTION ( 'NONE',  ( 0.000000000000000000, 0.000000000000000000, -1.000000000000000000 ) ) ;
#1208=CARTESIAN_POINT ( 'NONE',  ( -4.101948962585906244, 2.368261337751074169, -3.681124513963621503 ) ) ;
#1242=EDGE_CURVE ( 'NONE', #14765, #10609, #3913, .T. ) ;
#1244=CARTESIAN_POINT ( 'NONE',  ( 0.000000000000000000, 0.000000000000000000, -5.000000000000000000 ) ) ;
#1266=VERTEX_POINT ( 'NONE', #5715 ) ;
#1273=EDGE_CURVE ( 'NONE', #8664, #2509, #17299, .T. ) ;
#1276=EDGE_LOOP ( 'NONE', ( #15528, #6935, #13268, #10192 ) ) ;
#1289=CARTESIAN_POINT ( 'NONE',  ( 2.712762565639649015, -3.052587955997662306, -3.430618716626630871 ) ) ;
#1304=CARTESIAN_POINT ( 'NONE',  ( -3.511755186886750479, 2.826662030176366081, -3.597382984111578086 ) ) ;
#1308=CARTESIAN_POINT ( 'NONE',  ( -0.1410422978106123659, 4.700232962125094893, -3.687027686973624707 ) ) ;
#1369=ORIENTED_EDGE ( 'NONE', *, *, #5574, .F. ) ;
#1383=CARTESIAN_POINT ( 'NONE',  ( -6.259644161404860030E-16, -4.618802153517027165, -3.433295621305388234 ) ) ;
#1387=ADVANCED_FACE ( 'NONE', ( #17393 ), #16812, .F. ) ;
#1390=DIRECTION ( 'NONE',  ( 0.000000000000000000, 0.000000000000000000, -1.000000000000000000 ) ) ;
#1398=CARTESIAN_POINT ( 'NONE',  ( 2.100000000000000089, 0.000000000000000000, -0.2800830152838844622 ) ) ;
#1417=ORIENTED_EDGE ( 'NONE', *, *, #8421, .F. ) ;
#1421=CARTESIAN_POINT ( 'NONE',  ( 0.000000000000000000, 0.000000000000000000, -4.000000000000000000 ) ) ;
#1436=ORIENTED_EDGE ( 'NONE', *, *, #6062, .T. ) ;
#1466=CARTESIAN_POINT ( 'NONE',  ( 0.000000000000000000, 0.000000000000000000, 0.000000000000000000 ) ) ;
#1470=FACE_BOUND ( 'NONE', #952, .T. ) ;
#1474=CARTESIAN_POINT ( 'NONE',  ( 1.360585162435110629, -4.061296242128317857, -3.505054077164905024 ) ) ;
#1498=CARTESIAN_POINT ( 'NONE',  ( 4.000000000000000000, -2.309401076758514915, -3.433295621305383349 ) ) ;
#1500=CARTESIAN_POINT ( 'NONE',  ( 0.000000000000000000, 0.000000000000000000, -5.000000000000000000 ) ) ;
#1514=VERTEX_POINT ( 'NONE', #4538 ) ;
#1516=ORIENTED_EDGE ( 'NONE', *, *, #18984, .F. ) ;
#1553=( LENGTH_UNIT ( ) NAMED_UNIT ( * ) SI_UNIT ( .MILLI., .METRE. ) );
#1579=CIRCLE ( 'NONE', #3765, 4.000000000000000000 ) ;
#1595=CARTESIAN_POINT ( 'NONE',  ( 4.000000000000000000, 2.309401076758497151, -3.433295621305379353 ) ) ;
#1634=CARTESIAN_POINT ( 'NONE',  ( 3.511755186886750923, -2.826662030176382956, -3.597382984111582083 ) ) ;
#1659=CARTESIAN_POINT ( 'NONE',  ( -4.000000000000000000, 1.700094919196744270, -3.320312364301766017 ) ) ;
#1695=LINE ( 'NONE', #13350, #15160 ) ;
#1700=AXIS2_PLACEMENT_3D ( 'NONE', #15352, #5146, #453 ) ;
#1706=CARTESIAN_POINT ( 'NONE',  ( 2.100000000000000089, 0.000000000000000000, -4.694516984716113228 ) ) ;
#1707=EDGE_CURVE ( 'NONE', #3916, #848, #17010, .T. ) ;
#1722=ORIENTED_EDGE ( 'NONE', *, *, #10632, .F. ) ;
#1731=EDGE_CURVE ( 'NONE', #10976, #5141, #9505, .T. ) ;
#1748=VERTEX_POINT ( 'NONE', #795 ) ;
#1815=CARTESIAN_POINT ( 'NONE',  ( 0.3461262719736147297, -4.658553426539303821, -3.671615880910379381 ) ) ;
#1828=ORIENTED_EDGE ( 'NONE', *, *, #5909, .F. ) ;
#1830=ORIENTED_EDGE ( 'NONE', *, *, #9857, .F. ) ;
#1832=CARTESIAN_POINT ( 'NONE',  ( 3.349226789952652439, 2.685125164760731487, -0.2236248678334773199 ) ) ;
#1839=DIRECTION ( 'NONE',  ( 0.000000000000000000, -0.000000000000000000, 1.000000000000000000 ) ) ;
#1850=STYLED_ITEM ( 'NONE', ( #2135 ), #11045 ) ;
#1935=AXIS2_PLACEMENT_3D ( 'NONE', #996, #797, #8331 ) ;
#1941=CARTESIAN_POINT ( 'NONE',  ( 4.000000000000000000, -1.560351142792952617, -0.2242961665059816367 ) ) ;
#1999=ORIENTED_EDGE ( 'NONE', *, *, #3181, .F. ) ;
#2018=CARTESIAN_POINT ( 'NONE',  ( 0.000000000000000000, 0.000000000000000000, -4.000000000000000000 ) ) ;
#2024=ORIENTED_EDGE ( 'NONE', *, *, #11567, .F. ) ;
#2032=FACE_OUTER_BOUND ( 'NONE', #18602, .T. ) ;
#2068=DIRECTION ( 'NONE',  ( 0.000000000000000000, 0.000000000000000000, -1.000000000000000000 ) ) ;
#2093=VECTOR ( 'NONE', #10324, 1000.000000000000000 ) ;
#2109=ORIENTED_EDGE ( 'NONE', *, *, #6644, .T. ) ;
#2128=DIRECTION ( 'NONE',  ( -1.000000000000000000, 0.000000000000000000, 0.000000000000000000 ) ) ;
#2135=PRESENTATION_STYLE_ASSIGNMENT (( #15555 ) ) ;
#2154=DIRECTION ( 'NONE',  ( 1.000000000000000000, 0.000000000000000000, 0.000000000000000000 ) ) ;
#2157=( GEOMETRIC_REPRESENTATION_CONTEXT ( 3 ) GLOBAL_UNCERTAINTY_ASSIGNED_CONTEXT ( ( #6171 ) ) GLOBAL_UNIT_ASSIGNED_CONTEXT ( ( #10942, #5159, #17043 ) ) REPRESENTATION_CONTEXT ( 'NONE', 'WORKASPACE' ) );
#2169=FACE_OUTER_BOUND ( 'NONE', #6068, .T. ) ;
#2174=CARTESIAN_POINT ( 'NONE',  ( -2.449848172108560540, -3.432307619358754724, -3.503702292528910078 ) ) ;
#2185=ORIENTED_EDGE ( 'NONE', *, *, #9202, .T. ) ;
#2191=DIRECTION ( 'NONE',  ( 0.5000000000000022204, 0.8660254037844374864, -0.000000000000000000 ) ) ;
#2205=AXIS2_PLACEMENT_3D ( 'NONE', #12647, #15591, #592 ) ;
#2222=FACE_OUTER_BOUND ( 'NONE', #1276, .T. ) ;
#2232=CIRCLE ( 'NONE', #3769, 2.500000000000000888 ) ;
#2245=( NAMED_UNIT ( * ) PLANE_ANGLE_UNIT ( ) SI_UNIT ( $, .RADIAN. ) );
#2256=ORIENTED_EDGE ( 'NONE', *, *, #16352, .F. ) ;
#2263=CIRCLE ( 'NONE', #1935, 2.500000000000000444 ) ;
#2270=CARTESIAN_POINT ( 'NONE',  ( -4.000000000000000888, -1.539600717839011201, -3.300726591567081591 ) ) ;
#2275=DIRECTION ( 'NONE',  ( 1.000000000000000000, 0.000000000000000000, 0.000000000000000000 ) ) ;
#2276=CARTESIAN_POINT ( 'NONE',  ( -4.141042297810615835, 2.227970268150415656, -3.687027686973619822 ) ) ;
#2278=CARTESIAN_POINT ( 'NONE',  ( 0.6666666666666658525, -4.233901974057276085, -3.300726591567086476 ) ) ;
#2292=MANIFOLD_SOLID_BREP ( 'EndChamfer', #6791 ) ;
#2302=CARTESIAN_POINT ( 'NONE',  ( -2.855764796983342624, 2.970025579236414082, -0.09382832055445475272 ) ) ;
#2321=CARTESIAN_POINT ( 'NONE',  ( 4.000000000000000000, -2.309401076758516691, -0.4999999999999995559 ) ) ;
#2331=CARTESIAN_POINT ( 'NONE',  ( -1.240299975428134203E-15, -4.736529461165891242, -3.681130640444276292 ) ) ;
#2347=ADVANCED_FACE ( 'NONE', ( #13305 ), #16353, .F. ) ;
#2360=CARTESIAN_POINT ( 'NONE',  ( 4.000000000000000000, -2.511475576507276042, -3.469253905236643565 ) ) ;
#2393=CARTESIAN_POINT ( 'NONE',  ( 4.198928548860774157, -0.8158838809860124996, -3.526471437616918170 ) ) ;
#2394=EDGE_LOOP ( 'NONE', ( #2109, #16729, #3489, #1178 ) ) ;
#2402=AXIS2_PLACEMENT_3D ( 'NONE', #7221, #10062, #14374 ) ;
#2416=CARTESIAN_POINT ( 'NONE',  ( 4.211140560182196957, 2.431303136016536470, -3.745885042887433514 ) ) ;
#2464=EDGE_LOOP ( 'NONE', ( #7241, #7599, #2024 ) ) ;
#2465=CARTESIAN_POINT ( 'NONE',  ( 0.000000000000000000, 0.000000000000000000, 0.000000000000000000 ) ) ;
#2500=CARTESIAN_POINT ( 'NONE',  ( 3.540020015735602765, 2.810662092924382627, -3.602146406945867962 ) ) ;
#2509=VERTEX_POINT ( 'NONE', #10839 ) ;
#2515=CARTESIAN_POINT ( 'NONE',  ( -4.000000000000000000, 0.3987449864459974846, -0.01220643443059782861 ) ) ;
#2573=DIRECTION ( 'NONE',  ( 1.000000000000000000, 0.000000000000000000, 0.000000000000000000 ) ) ;
#2604=EDGE_CURVE ( 'NONE', #5450, #10423, #15096, .T. ) ;
#2623=B_SPLINE_CURVE_WITH_KNOTS ( 'NONE', 3,
 ( #6898, #11496, #2515, #18981, #5137, #17505, #11108, #17115 ),
 .UNSPECIFIED., .F., .F.,
 ( 4, 2, 2, 4 ),
 ( 0.005725059856848641743, 0.006314084072593626612, 0.006903108288338611481, 0.008081156719828581220 ),
 .UNSPECIFIED. ) ;
#2624=CARTESIAN_POINT ( 'NONE',  ( 2.687328764639642653, -3.067272167851299969, -0.05923475698271395140 ) ) ;
#2664=FACE_OUTER_BOUND ( 'NONE', #10436, .T. ) ;
#2684=CARTESIAN_POINT ( 'NONE',  ( -3.453038570459499024, -2.625189405340453419, -3.535263753545272891 ) ) ;
#2688=CARTESIAN_POINT ( 'NONE',  ( 4.197393957002303999, 7.772902908466098641E-14, -3.503767560748929810 ) ) ;
#2691=CARTESIAN_POINT ( 'NONE',  ( 2.756197834950227410, 3.027510591568626896, -3.223146290109805356 ) ) ;
#2709=CARTESIAN_POINT ( 'NONE',  ( 0.000000000000000000, 0.000000000000000000, -4.974599999999998801 ) ) ;
#2710=EDGE_CURVE ( 'NONE', #442, #5017, #9444, .T. ) ;
#2739=CARTESIAN_POINT ( 'NONE',  ( -0.5469614295416921346, 4.303013824936271270, -3.535263753543735454 ) ) ;
#2741=DIRECTION ( 'NONE',  ( 1.000000000000000000, 0.000000000000000000, 0.000000000000000000 ) ) ;
#2759=ADVANCED_FACE ( 'NONE', ( #8600 ), #5931, .F. ) ;
#2786=CARTESIAN_POINT ( 'NONE',  ( -4.000000000000004441, 2.309401076758496263, -3.504269196027523847 ) ) ;
#2804=FACE_OUTER_BOUND ( 'NONE', #13318, .T. ) ;
#2844=CARTESIAN_POINT ( 'NONE',  ( -2.688821387764050996E-14, -4.618802153517012954, -0.4999999999999995559 ) ) ;
#2871=CARTESIAN_POINT ( 'NONE',  ( 0.000000000000000000, 0.000000000000000000, 0.000000000000000000 ) ) ;
#2876=EDGE_CURVE ( 'NONE', #162, #9683, #13779, .T. ) ;
#2931=( NAMED_UNIT ( * ) PLANE_ANGLE_UNIT ( ) SI_UNIT ( $, .RADIAN. ) );
#2936=ORIENTED_EDGE ( 'NONE', *, *, #6489, .T. ) ;
#2940=VERTEX_POINT ( 'NONE', #7703 ) ;
#2943=EDGE_CURVE ( 'NONE', #7410, #9683, #9451, .T. ) ;
#2947=DIRECTION ( 'NONE',  ( 0.000000000000000000, 0.000000000000000000, 1.000000000000000000 ) ) ;
#2969=CARTESIAN_POINT ( 'NONE',  ( -1.393927851585477606, 4.043713361053528743, -3.526374918436835149 ) ) ;
#2994=CARTESIAN_POINT ( 'NONE',  ( 2.000000000000008882, 3.464101615137749945, 0.000000000000000000 ) ) ;
#3011=DIRECTION ( 'NONE',  ( 1.000000000000000000, 0.000000000000000000, 0.000000000000000000 ) ) ;
#3074=CARTESIAN_POINT ( 'NONE',  ( -6.473970235329672780E-16, -4.862606272033106691, -3.745885042887442395 ) ) ;
#3105=CARTESIAN_POINT ( 'NONE',  ( -3.333333333333335258, 2.694301256218251783, -3.300726591567079815 ) ) ;
#3116=ADVANCED_FACE ( 'NONE', ( #643 ), #18619, .T. ) ;
#3131=CARTESIAN_POINT ( 'NONE',  ( -4.197312064133472020, -0.8182229787990021874, -3.502518405183886685 ) ) ;
#3181=EDGE_CURVE ( 'NONE', #1266, #14141, #11772, .T. ) ;
#3185=CARTESIAN_POINT ( 'NONE',  ( 4.211140560182196957, 2.431303136016536470, -3.745885042887433514 ) ) ;
#3188=ADVANCED_FACE ( 'NONE', ( #2804 ), #14830, .T. ) ;
#3247=CARTESIAN_POINT ( 'NONE',  ( 0.5469614295415388128, -4.303013824935362663, -3.535263753543555598 ) ) ;
#3268=CARTESIAN_POINT ( 'NONE',  ( 4.197393957002303999, 0.8151795401431359833, -3.503767560748935139 ) ) ;
#3284=CARTESIAN_POINT ( 'NONE',  ( -4.211140560182196957, -2.431303136016552013, -3.745885042887436178 ) ) ;
#3296=( BOUNDED_SURFACE ( )  B_SPLINE_SURFACE ( 3, 2, ( 
 ( #11832, #13307, #13511 ),
 ( #1659, #19324, #11733 ),
 ( #4295, #5863, #7622 ),
 ( #17837, #17941, #3131 ),
 ( #4592, #4398, #10365 ),
 ( #19227, #8989, #6150 ) ),
 .UNSPECIFIED., .F., .F., .F. ) 
 B_SPLINE_SURFACE_WITH_KNOTS ( ( 4, 2, 4 ),
 ( 3, 3 ),
 ( 0.02027752710269158445, 0.02273781595091097299, 0.02519810479913036153 ),
 ( 0.000000000000000000, 1.000000000000000000 ),
 .UNSPECIFIED. ) 
 GEOMETRIC_REPRESENTATION_ITEM ( )  RATIONAL_B_SPLINE_SURFACE ( (
 ( 1.000000000000000000, 0.8047781431712808242, 1.000000000000000000),
 ( 1.000000000000000000, 0.8123773247083928561, 1.000000000000000000),
 ( 1.000000000000000000, 0.8190670192154906326, 1.000000000000000000),
 ( 1.000000000000000000, 0.8192353552912178261, 1.000000000000000000),
 ( 1.000000000000000000, 0.8126132098226825917, 1.000000000000000000),
 ( 1.000000000000000000, 0.8047712465856394770, 1.000000000000000000) ) ) 
 REPRESENTATION_ITEM ( '' )  SURFACE ( )  );
#3384=ORIENTED_EDGE ( 'NONE', *, *, #9540, .T. ) ;
#3387=B_SPLINE_CURVE_WITH_KNOTS ( 'NONE', 3,
 ( #5744, #14854, #8680, #3105, #13381 ),
 .UNSPECIFIED., .F., .F.,
 ( 4, 1, 4 ),
 ( 0.000000000000000000, 0.002309401076758506657, 0.004618802153517013315 ),
 .UNSPECIFIED. ) ;
#3420=DIRECTION ( 'NONE',  ( 1.000000000000000000, 0.000000000000000000, 0.000000000000000000 ) ) ;
#3471=ORIENTED_EDGE ( 'NONE', *, *, #10471, .T. ) ;
#3489=ORIENTED_EDGE ( 'NONE', *, *, #1242, .F. ) ;
#3490=LINE ( 'NONE', #14052, #9084 ) ;
#3533=DIRECTION ( 'NONE',  ( 1.000000000000000000, 0.000000000000000000, 0.000000000000000000 ) ) ;
#3557=FACE_OUTER_BOUND ( 'NONE', #18685, .T. ) ;
#3569=ADVANCED_FACE ( 'NONE', ( #9335 ), #4842, .T. ) ;
#3570=CARTESIAN_POINT ( 'NONE',  ( -4.203833317240879275, -1.627343821129593859, -3.597273115243890818 ) ) ;
#3577=B_SPLINE_CURVE_WITH_KNOTS ( 'NONE', 3,
 ( #83, #15166, #1941, #15255, #9361, #9082 ),
 .UNSPECIFIED., .F., .F.,
 ( 4, 2, 4 ),
 ( 0.003358874760055551890, 0.004541967308452098118, 0.005725059856848645212 ),
 .UNSPECIFIED. ) ;
#3596=CARTESIAN_POINT ( 'NONE',  ( 0.000000000000000000, 0.000000000000000000, 3.469446951953614189E-15 ) ) ;
#3622=MECHANICAL_DESIGN_GEOMETRIC_PRESENTATION_REPRESENTATION('',(#6750),#808);
#3626=LINE ( 'NONE', #7934, #10493 ) ;
#3636=CARTESIAN_POINT ( 'NONE',  ( -0.6920835326022555245, -4.454600218803899558, -3.597382984111586079 ) ) ;
#3662=CARTESIAN_POINT ( 'NONE',  ( -4.000000000000000000, 2.309401076758498483, -0.4999999999999927280 ) ) ;
#3692=CARTESIAN_POINT ( 'NONE',  ( -4.000000000000000000, -0.3979232138631226823, -3.896351557369779711E-17 ) ) ;
#3698=SURFACE_SIDE_STYLE ('',( #12515 ) ) ;
#3765=AXIS2_PLACEMENT_3D ( 'NONE', #6190, #9408, #15301 ) ;
#3766=EDGE_LOOP ( 'NONE', ( #6274, #11337, #16028, #14176, #7839 ) ) ;
#3769=AXIS2_PLACEMENT_3D ( 'NONE', #10862, #18440, #4987 ) ;
#3776=AXIS2_PLACEMENT_3D ( 'NONE', #4245, #4545, #4452 ) ;
#3777=ORIENTED_EDGE ( 'NONE', *, *, #18984, .T. ) ;
#3778=CARTESIAN_POINT ( 'NONE',  ( 3.999999999999999112, 2.309401076758497595, -3.504271511726784194 ) ) ;
#3824=CARTESIAN_POINT ( 'NONE',  ( 4.197478902586992966, -0.8524102783748346290, -3.505063281295504041 ) ) ;
#3833=CARTESIAN_POINT ( 'NONE',  ( 0.000000000000000000, 0.000000000000000000, 0.000000000000000000 ) ) ;
#3852=ORIENTED_EDGE ( 'NONE', *, *, #6062, .F. ) ;
#3884=DIRECTION ( 'NONE',  ( -1.000000000000000000, 0.000000000000000000, 0.000000000000000000 ) ) ;
#3913=B_SPLINE_CURVE_WITH_KNOTS ( 'NONE', 3,
 ( #18291, #6317, #6594, #9529, #4844, #15520 ),
 .UNSPECIFIED., .F., .F.,
 ( 4, 2, 4 ),
 ( 4.336808689942017736E-19, 0.0002095117440854729585, 0.0004190234881709454834 ),
 .UNSPECIFIED. ) ;
#3916=VERTEX_POINT ( 'NONE', #3074 ) ;
#3953=CARTESIAN_POINT ( 'NONE',  ( 4.175002511812151873, 2.208363329454889445, -3.469254087858244073 ) ) ;
#3982=CARTESIAN_POINT ( 'NONE',  ( 2.804994570502171047, 3.229033611042449792, -3.526374918436834704 ) ) ;
#4022=AXIS2_PLACEMENT_3D ( 'NONE', #18643, #6659, #3533 ) ;
#4052=CARTESIAN_POINT ( 'NONE',  ( 3.472371940585993855, 2.614027278893175321, -3.320322319201766792 ) ) ;
#4068=CARTESIAN_POINT ( 'NONE',  ( 4.211140560182196957, 2.431303136016536470, -3.745885042887433514 ) ) ;
#4099=ORIENTED_EDGE ( 'NONE', *, *, #10632, .T. ) ;
#4177=DIRECTION ( 'NONE',  ( 1.224646799147353207E-16, 1.000000000000000000, 0.000000000000000000 ) ) ;
#4184=CYLINDRICAL_SURFACE ( 'NONE', #17508, 2.100000000000000089 ) ;
#4187=LINE ( 'NONE', #13008, #15668 ) ;
#4193=CARTESIAN_POINT ( 'NONE',  ( 0.02448733951239481094, 4.877042772274728044, -3.751161874094022242 ) ) ;
#4208=ORIENTED_EDGE ( 'NONE', *, *, #18395, .F. ) ;
#4230=CARTESIAN_POINT ( 'NONE',  ( 0.1410422978106145031, -4.700232962125109104, -3.687027686973628704 ) ) ;
#4245=CARTESIAN_POINT ( 'NONE',  ( 0.000000000000000000, 0.000000000000000000, 3.469446951953614189E-15 ) ) ;
#4263=AXIS2_PLACEMENT_3D ( 'NONE', #17655, #9885, #13222 ) ;
#4265=EDGE_CURVE ( 'NONE', #8664, #14765, #12994, .T. ) ;
#4267=DIRECTION ( 'NONE',  ( 0.000000000000000000, 0.000000000000000000, 1.000000000000000000 ) ) ;
#4295=CARTESIAN_POINT ( 'NONE',  ( -4.000000000000000000, 0.8730739991738342143, -3.223134629628428893 ) ) ;
#4305=ORIENTED_EDGE ( 'NONE', *, *, #5425, .F. ) ;
#4307=DIRECTION ( 'NONE',  ( -1.000000000000000000, 0.000000000000000000, 0.000000000000000000 ) ) ;
#4318=CARTESIAN_POINT ( 'NONE',  ( 3.455068668934414777, -2.624017327439094327, -3.316620875263732504 ) ) ;
#4328=CARTESIAN_POINT ( 'NONE',  ( 0.1756481739660539498, -4.720212674038995360, -3.469390959564070620 ) ) ;
#4363=ADVANCED_FACE ( 'NONE', ( #1470, #7449 ), #5690, .T. ) ;
#4389=CARTESIAN_POINT ( 'NONE',  ( -2.712762565639006418, 3.052587955997511759, -3.430618716626627318 ) ) ;
#4398=CARTESIAN_POINT ( 'NONE',  ( -3.999999999998910649, -1.658469974638591804, -3.531532913075256186 ) ) ;
#4402=CARTESIAN_POINT ( 'NONE',  ( -2.000000000000007550, -3.464101615137749945, 0.000000000000000000 ) ) ;
#4452=DIRECTION ( 'NONE',  ( 1.000000000000000000, 0.000000000000000000, 0.000000000000000000 ) ) ;
#4460=ORIENTED_EDGE ( 'NONE', *, *, #5778, .F. ) ;
#4480=CARTESIAN_POINT ( 'NONE',  ( -1.828356344711647319, -3.563200125723192002, -1.076197711133951296E-14 ) ) ;
#4504=CARTESIAN_POINT ( 'NONE',  ( -1.312671235360383548, -3.860931062424228788, -0.05923475698271369466 ) ) ;
#4521=CARTESIAN_POINT ( 'NONE',  ( 4.236525694536557474, -2.416953475386482530, -3.751298745799839462 ) ) ;
#4538=CARTESIAN_POINT ( 'NONE',  ( -4.000000000000000000, -2.309401076758515803, -0.4999999999999995559 ) ) ;
#4545=DIRECTION ( 'NONE',  ( -0.000000000000000000, -0.000000000000000000, 1.000000000000000000 ) ) ;
#4547=ORIENTED_EDGE ( 'NONE', *, *, #5091, .T. ) ;
#4556=AXIS2_PLACEMENT_3D ( 'NONE', #10834, #6145, #9183 ) ;
#4558=ORIENTED_EDGE ( 'NONE', *, *, #10222, .T. ) ;
#4592=CARTESIAN_POINT ( 'NONE',  ( -4.000000000000000000, -1.680117682357936904, -3.316611593218794951 ) ) ;
#4594=EDGE_LOOP ( 'NONE', ( #3777, #5571, #17551 ) ) ;
#4653=CARTESIAN_POINT ( 'NONE',  ( 0.3208286057739604957, -4.433571671609698228, -0.3503314178412692548 ) ) ;
#4702=CARTESIAN_POINT ( 'NONE',  ( -4.000000000000000888, -2.309401076758512694, -3.504269196027526512 ) ) ;
#4708=CARTESIAN_POINT ( 'NONE',  ( -5.560781378645575757, 6.809993116116508640E-16, -4.000000000000000000 ) ) ;
#4743=CARTESIAN_POINT ( 'NONE',  ( -4.197393957002303999, -7.773935952363655451E-14, -3.503767560748929810 ) ) ;
#4764=CARTESIAN_POINT ( 'NONE',  ( -4.197393957002303999, -7.773935952363655451E-14, -3.503767560748929810 ) ) ;
#4786=DIRECTION ( 'NONE',  ( 1.000000000000000000, 0.000000000000000000, 0.000000000000000000 ) ) ;
#4790=VERTEX_POINT ( 'NONE', #18631 ) ;
#4842=PLANE ( 'NONE',  #15789 ) ;
#4844=CARTESIAN_POINT ( 'NONE',  ( 4.154306624731035846, -2.398490048085128556, -3.721999068284417955 ) ) ;
#4906=AXIS2_PLACEMENT_3D ( 'NONE', #1421, #7585, #10517 ) ;
#4912=AXIS2_PLACEMENT_3D ( 'NONE', #9524, #2191, #336 ) ;
#4913=CARTESIAN_POINT ( 'NONE',  ( -2.804994570502171047, -3.229033611042465335, -3.526374918436838701 ) ) ;
#4927=CARTESIAN_POINT ( 'NONE',  ( -4.000000000000000000, 2.309401076758498483, -5.000000000000000000 ) ) ;
#4946=DIRECTION ( 'NONE',  ( -0.000000000000000000, -0.000000000000000000, 1.000000000000000000 ) ) ;
#4987=DIRECTION ( 'NONE',  ( 1.000000000000000000, 0.000000000000000000, 0.000000000000000000 ) ) ;
#5003=UNCERTAINTY_MEASURE_WITH_UNIT (LENGTH_MEASURE( 1.000000000000000082E-05 ), #1553, 'distance_accuracy_value', 'NONE');
#5017=VERTEX_POINT ( 'NONE', #18588 ) ;
#5023=AXIS2_PLACEMENT_3D ( 'NONE', #2018, #4946, #9352 ) ;
#5043=ORIENTED_EDGE ( 'NONE', *, *, #14825, .F. ) ;
#5061=CARTESIAN_POINT ( 'NONE',  ( 0.6920835326022565237, 4.454600218803884459, -3.597382984111579862 ) ) ;
#5072=VERTEX_POINT ( 'NONE', #9624 ) ;
#5091=EDGE_CURVE ( 'NONE', #18115, #1014, #16980, .T. ) ;
#5137=CARTESIAN_POINT ( 'NONE',  ( -4.000000000000000000, 0.9868501483902560878, -0.09357334158579519445 ) ) ;
#5141=VERTEX_POINT ( 'NONE', #9086 ) ;
#5146=DIRECTION ( 'NONE',  ( 0.000000000000000000, 0.000000000000000000, -1.000000000000000000 ) ) ;
#5149=CARTESIAN_POINT ( 'NONE',  ( -6.259644161404860030E-16, -4.618802153517027165, -5.000000000000000000 ) ) ;
#5159=( NAMED_UNIT ( * ) PLANE_ANGLE_UNIT ( ) SI_UNIT ( $, .RADIAN. ) );
#5190=CARTESIAN_POINT ( 'NONE',  ( -0.5276280594146446346, 4.314175951381965746, -3.320322319201721495 ) ) ;
#5198=LINE ( 'NONE', #6672, #10994 ) ;
#5206=ORIENTED_EDGE ( 'NONE', *, *, #12263, .F. ) ;
#5239=CARTESIAN_POINT ( 'NONE',  ( -1.655952806101422814, 3.662737355149034979, -7.623296525288699970E-18 ) ) ;
#5271=CARTESIAN_POINT ( 'NONE',  ( 4.000000000000000888, 1.563622288139206118, -0.2253451193528334950 ) ) ;
#5281=CARTESIAN_POINT ( 'NONE',  ( 4.204115023516791005, -1.660442669500199919, -3.602151381774560068 ) ) ;
#5329=EDGE_CURVE ( 'NONE', #14765, #162, #10899, .T. ) ;
#5336=B_SPLINE_CURVE_WITH_KNOTS ( 'NONE', 3,
 ( #10393, #10580, #9015, #204, #16393, #17866 ),
 .UNSPECIFIED., .F., .F.,
 ( 4, 2, 4 ),
 ( 0.002452478801916376308, 0.003676905084148007850, 0.004901331366379639391 ),
 .UNSPECIFIED. ) ;
#5342=ORIENTED_EDGE ( 'NONE', *, *, #9144, .F. ) ;
#5343=CARTESIAN_POINT ( 'NONE',  ( 0.000000000000000000, 0.000000000000000000, -5.000000000000000000 ) ) ;
#5346=CONICAL_SURFACE ( 'NONE', #6287, 4.000000000000000000, 0.8911886515913786111 ) ;
#5383=CARTESIAN_POINT ( 'NONE',  ( 3.999999999999998224, 2.472263674411418588, -3.687027874309861897 ) ) ;
#5403=VERTEX_POINT ( 'NONE', #124 ) ;
#5412=CARTESIAN_POINT ( 'NONE',  ( -6.259644161404860030E-16, -4.618802153517027165, -5.000000000000000000 ) ) ;
#5425=EDGE_CURVE ( 'NONE', #11229, #10265, #1695, .T. ) ;
#5450=VERTEX_POINT ( 'NONE', #10499 ) ;
#5484=B_SPLINE_CURVE_WITH_KNOTS ( 'NONE', 3,
 ( #46, #11993, #13565, #14740, #4653, #5827 ),
 .UNSPECIFIED., .F., .F.,
 ( 4, 2, 4 ),
 ( 0.002365888236227967761, 0.003551327329835077609, 0.004736766423442186590 ),
 .UNSPECIFIED. ) ;
#5499=CARTESIAN_POINT ( 'NONE',  ( 4.000000000000000000, 2.309401076758497151, -3.433295621305379353 ) ) ;
#5508=DIRECTION ( 'NONE',  ( 0.000000000000000000, 0.000000000000000000, 1.000000000000000000 ) ) ;
#5539=DIRECTION ( 'NONE',  ( -1.000000000000000000, 1.224646799147352714E-16, 0.000000000000000000 ) ) ;
#5541=ORIENTED_EDGE ( 'NONE', *, *, #18395, .T. ) ;
#5571=ORIENTED_EDGE ( 'NONE', *, *, #13634, .F. ) ;
#5572=LINE ( 'NONE', #9973, #9642 ) ;
#5574=EDGE_CURVE ( 'NONE', #18909, #4790, #5198, .T. ) ;
#5582=ORIENTED_EDGE ( 'NONE', *, *, #11774, .F. ) ;
#5591=MECHANICAL_DESIGN_GEOMETRIC_PRESENTATION_REPRESENTATION('',(#1850),#2157);
#5592=FACE_OUTER_BOUND ( 'NONE', #2394, .T. ) ;
#5601=CARTESIAN_POINT ( 'NONE',  ( 2.000000000000000444, 3.464101615137754830, -3.142992957459231018 ) ) ;
#5615=CARTESIAN_POINT ( 'NONE',  ( -4.154094228333456762, 2.398367420968013253, -3.721909803043220055 ) ) ;
#5653=LINE ( 'NONE', #11628, #18192 ) ;
#5680=ORIENTED_EDGE ( 'NONE', *, *, #2943, .F. ) ;
#5685=ORIENTED_EDGE ( 'NONE', *, *, #4265, .T. ) ;
#5690=PLANE ( 'NONE',  #12982 ) ;
#5715=CARTESIAN_POINT ( 'NONE',  ( 4.000000000000000000, -2.309401076758516691, -0.4999999999999995559 ) ) ;
#5744=CARTESIAN_POINT ( 'NONE',  ( 1.567478505476134606E-15, 4.618802153517012066, -3.433295621305382905 ) ) ;
#5765=DIRECTION ( 'NONE',  ( -0.000000000000000000, -0.000000000000000000, 1.000000000000000000 ) ) ;
#5769=EDGE_LOOP ( 'NONE', ( #1828, #8505, #1516, #11021, #16379, #9093 ) ) ;
#5778=EDGE_CURVE ( 'NONE', #16922, #16847, #2263, .T. ) ;
#5827=CARTESIAN_POINT ( 'NONE',  ( -2.688821387764050996E-14, -4.618802153517012954, -0.4999999999999995559 ) ) ;
#5845=ADVANCED_FACE ( 'NONE', ( #5592 ), #7299, .F. ) ;
#5863=CARTESIAN_POINT ( 'NONE',  ( -4.000000000000000000, 0.8576368993457507139, -3.433240632782198709 ) ) ;
#5874=CARTESIAN_POINT ( 'NONE',  ( 0.000000000000000000, 0.000000000000000000, 0.000000000000000000 ) ) ;
#5877=CARTESIAN_POINT ( 'NONE',  ( -4.211140560182196957, -2.431303136016552013, -3.745885042887436178 ) ) ;
#5887=CARTESIAN_POINT ( 'NONE',  ( 0.6640947660595348800, -4.471078309994175548, -3.602146406945708090 ) ) ;
#5895=ORIENTED_EDGE ( 'NONE', *, *, #12720, .T. ) ;
#5896=CARTESIAN_POINT ( 'NONE',  ( -3.540020015735593439, -2.810662092924100630, -3.602146406945814672 ) ) ;
#5909=EDGE_CURVE ( 'NONE', #8263, #1014, #8138, .T. ) ;
#5931=( BOUNDED_SURFACE ( )  B_SPLINE_SURFACE ( 3, 2, ( 
 ( #14571, #15695, #4193 ),
 ( #5190, #2739, #17540 ),
 ( #11634, #13109, #7229 ),
 ( #8696, #4389, #9695 ),
 ( #17643, #10255, #19317 ),
 ( #17170, #2276, #14670 ) ),
 .UNSPECIFIED., .F., .F., .T. ) 
 B_SPLINE_SURFACE_WITH_KNOTS ( ( 4, 2, 4 ),
 ( 3, 3 ),
 ( 0.02032853247518125531, 0.02278863295364820865, 0.02524873343211516200 ),
 ( 0.000000000000000000, 1.000000000000000000 ),
 .UNSPECIFIED. ) 
 GEOMETRIC_REPRESENTATION_ITEM ( )  RATIONAL_B_SPLINE_SURFACE ( (
 ( 1.000000000000000000, 0.8047781615896836271, 1.000000000000000000),
 ( 1.000000000000000000, 0.8123767586289967202, 1.000000000000000000),
 ( 1.000000000000000000, 0.8190662415563443322, 1.000000000000000000),
 ( 1.000000000000000000, 0.8192361015669982205, 1.000000000000000000),
 ( 1.000000000000000000, 0.8126135807103181952, 1.000000000000000000),
 ( 1.000000000000000000, 0.8047712338318587788, 1.000000000000000000) ) ) 
 REPRESENTATION_ITEM ( '' )  SURFACE ( )  );
#5949=DIRECTION ( 'NONE',  ( 0.000000000000000000, 0.000000000000000000, 1.000000000000000000 ) ) ;
#5967=B_SPLINE_CURVE_WITH_KNOTS ( 'NONE', 3,
 ( #11380, #1304, #16198, #7273, #2969, #6975, #13152, #14613 ),
 .UNSPECIFIED., .F., .F.,
 ( 4, 2, 2, 4 ),
 ( 0.000000000000000000, 0.002450665683189820997, 0.003675998524784731495, 0.004901331366379641993 ),
 .UNSPECIFIED. ) ;
#5976=AXIS2_PLACEMENT_3D ( 'NONE', #13897, #9206, #2154 ) ;
#6012=AXIS2_PLACEMENT_3D ( 'NONE', #7430, #5765, #17737 ) ;
#6016=CARTESIAN_POINT ( 'NONE',  ( 4.000000000000000888, 1.539600717838996990, -3.300726591567079815 ) ) ;
#6058=PLANE ( 'NONE',  #19287 ) ;
#6062=EDGE_CURVE ( 'NONE', #7928, #10265, #12537, .T. ) ;
#6068=EDGE_LOOP ( 'NONE', ( #4305, #15464, #9179, #15341, #14394, #9518, #1436 ) ) ;
#6096=EDGE_CURVE ( 'NONE', #16847, #2940, #18546, .T. ) ;
#6114=CARTESIAN_POINT ( 'NONE',  ( -3.974344831685191280E-13, 4.796734841935104576, -3.721909803043223608 ) ) ;
#6145=DIRECTION ( 'NONE',  ( -0.000000000000000000, -0.000000000000000000, 1.000000000000000000 ) ) ;
#6150=CARTESIAN_POINT ( 'NONE',  ( -4.211405944401398038, -2.460460786169389902, -3.751298493805494072 ) ) ;
#6163=EDGE_CURVE ( 'NONE', #5141, #2940, #2232, .T. ) ;
#6171=UNCERTAINTY_MEASURE_WITH_UNIT (LENGTH_MEASURE( 1.000000000000000082E-05 ), #10942, 'distance_accuracy_value', 'NONE');
#6181=CARTESIAN_POINT ( 'NONE',  ( -4.000000000000000000, -0.7890432684750890990, -0.04868663549882315533 ) ) ;
#6190=CARTESIAN_POINT ( 'NONE',  ( 0.000000000000000000, 0.000000000000000000, 0.000000000000000000 ) ) ;
#6207=CARTESIAN_POINT ( 'NONE',  ( 2.100000000000000089, 0.000000000000000000, -5.000000000000000000 ) ) ;
#6256=CARTESIAN_POINT ( 'NONE',  ( -4.000000000000000000, -2.309401076758512694, -3.433295621305382461 ) ) ;
#6262=DIRECTION ( 'NONE',  ( -1.000000000000000000, 0.000000000000000000, 0.000000000000000000 ) ) ;
#6274=ORIENTED_EDGE ( 'NONE', *, *, #8736, .F. ) ;
#6287=AXIS2_PLACEMENT_3D ( 'NONE', #3833, #2068, #9795 ) ;
#6317=CARTESIAN_POINT ( 'NONE',  ( 4.000000000000003553, -2.309401076758513138, -3.504271511726786859 ) ) ;
#6324=DIRECTION ( 'NONE',  ( 0.000000000000000000, 0.000000000000000000, 1.000000000000000000 ) ) ;
#6334=ORIENTED_EDGE ( 'NONE', *, *, #11774, .T. ) ;
#6408=ADVANCED_FACE ( 'NONE', ( #14875 ), #3296, .F. ) ;
#6489=EDGE_CURVE ( 'NONE', #16847, #16922, #16953, .T. ) ;
#6499=CARTESIAN_POINT ( 'NONE',  ( 0.6937372685066666156, -4.453844082567737672, -3.610536846335894445 ) ) ;
#6501=ORIENTED_EDGE ( 'NONE', *, *, #1707, .F. ) ;
#6512=AXIS2_PLACEMENT_3D ( 'NONE', #10867, #12343, #12438 ) ;
#6518=EDGE_CURVE ( 'NONE', #12905, #9774, #7851, .T. ) ;
#6573=CIRCLE ( 'NONE', #5023, 5.560781378645573980 ) ;
#6594=CARTESIAN_POINT ( 'NONE',  ( 4.024499207728657879, -2.323545700935587988, -3.572172305156509964 ) ) ;
#6602=PLANE ( 'NONE',  #325 ) ;
#6628=CARTESIAN_POINT ( 'NONE',  ( -6.473970235329672780E-16, -4.862606272033106691, -3.745885042887442395 ) ) ;
#6636=EDGE_CURVE ( 'NONE', #5403, #10751, #18481, .T. ) ;
#6644=EDGE_CURVE ( 'NONE', #8664, #3916, #14707, .T. ) ;
#6659=DIRECTION ( 'NONE',  ( -0.000000000000000000, -0.000000000000000000, 1.000000000000000000 ) ) ;
#6664=VERTEX_POINT ( 'NONE', #746 ) ;
#6672=CARTESIAN_POINT ( 'NONE',  ( 1.567478505476134606E-15, 4.618802153517012066, -5.000000000000000000 ) ) ;
#6676=DIRECTION ( 'NONE',  ( -1.000000000000000000, 0.000000000000000000, 0.000000000000000000 ) ) ;
#6685=LINE ( 'NONE', #4927, #14612 ) ;
#6695=AXIS2_PLACEMENT_3D ( 'NONE', #10041, #14354, #8765 ) ;
#6729=EDGE_LOOP ( 'NONE', ( #7611, #4099, #14653, #11149 ) ) ;
#6747=CARTESIAN_POINT ( 'NONE',  ( 4.211399257449709665, -2.459727064652517114, -3.751161691472417736 ) ) ;
#6750=STYLED_ITEM('',(#19475),#2292);
#6773=CONICAL_SURFACE ( 'NONE', #4906, 5.560781378645573980, 1.221730476396046816 ) ;
#6791=CLOSED_SHELL ( 'NONE', ( #8240, #10768, #2347, #7363, #11435, #10168, #15494, #14396, #12169, #17554, #8540, #3569, #18761, #512, #4363, #3188, #17086, #8563, #15078, #9604, #17238, #410, #3116, #9169, #5845, #6408, #13465, #2759, #1387, #522, #11583, #17549 ) ) ;
#6797=DIRECTION ( 'NONE',  ( -0.8660254037844377084, -0.5000000000000015543, 0.000000000000000000 ) ) ;
#6806=DIRECTION ( 'NONE',  ( 1.000000000000000000, 0.000000000000000000, 0.000000000000000000 ) ) ;
#6816=VECTOR ( 'NONE', #4267, 1000.000000000000000 ) ;
#6844=CARTESIAN_POINT ( 'NONE',  ( 4.203935335434060505, 1.640780671294165272, -3.598452447879202598 ) ) ;
#6876=EDGE_LOOP ( 'NONE', ( #5582, #10088 ) ) ;
#6884=B_SPLINE_CURVE_WITH_KNOTS ( 'NONE', 3,
 ( #16188, #14508, #14804, #17666, #1383 ),
 .UNSPECIFIED., .F., .F.,
 ( 4, 1, 4 ),
 ( 0.000000000000000000, 0.002309401076758505356, 0.004618802153517010713 ),
 .UNSPECIFIED. ) ;
#6898=CARTESIAN_POINT ( 'NONE',  ( -4.000000000000000000, 0.000000000000000000, 0.000000000000000000 ) ) ;
#6903=ORIENTED_EDGE ( 'NONE', *, *, #15883, .F. ) ;
#6935=ORIENTED_EDGE ( 'NONE', *, *, #9621, .T. ) ;
#6944=PRODUCT ( 'hex flange nut gradea_iso_ISO - 4161 - M5 - N', 'hex flange nut gradea_iso_ISO - 4161 - M5 - N', '', ( #17972 ) ) ;
#6948=DIRECTION ( 'NONE',  ( -0.8191520442889902442, 0.000000000000000000, -0.5735764363510482688 ) ) ;
#6975=CARTESIAN_POINT ( 'NONE',  ( -0.6937372685066653943, 4.453844082567723461, -3.610536846335889116 ) ) ;
#6979=CARTESIAN_POINT ( 'NONE',  ( 0.5449313310647804220, 4.304185902836899835, -3.316620875263383894 ) ) ;
#6997=DIRECTION ( 'NONE',  ( -1.000000000000000000, 0.000000000000000000, 0.000000000000000000 ) ) ;
#7011=EDGE_CURVE ( 'NONE', #848, #19213, #16802, .T. ) ;
#7013=EDGE_CURVE ( 'NONE', #10609, #3916, #1142, .T. ) ;
#7025=EDGE_LOOP ( 'NONE', ( #9165, #18891, #7715, #13289, #1417 ) ) ;
#7027=FACE_OUTER_BOUND ( 'NONE', #6729, .T. ) ;
#7047=ORIENTED_EDGE ( 'NONE', *, *, #1273, .F. ) ;
#7055=CARTESIAN_POINT ( 'NONE',  ( 1.999999999999998224, -3.464101615137772594, -3.142992957459239012 ) ) ;
#7068=CARTESIAN_POINT ( 'NONE',  ( 5.384454397937118664, 0.000000000000000000, -4.484454397937119197 ) ) ;
#7156=DIRECTION ( 'NONE',  ( -1.000000000000000000, 0.000000000000000000, 0.000000000000000000 ) ) ;
#7221=CARTESIAN_POINT ( 'NONE',  ( 0.000000000000000000, 0.000000000000000000, -5.000000000000000000 ) ) ;
#7228=EDGE_LOOP ( 'NONE', ( #11490, #10627, #9960, #15326, #749 ) ) ;
#7229=CARTESIAN_POINT ( 'NONE',  ( -1.360585162435467455, 4.061296242128285883, -3.505054077164959203 ) ) ;
#7241=ORIENTED_EDGE ( 'NONE', *, *, #17571, .T. ) ;
#7271=CARTESIAN_POINT ( 'NONE',  ( -2.742827927723112236, -3.035229711105190464, -3.433252694550595230 ) ) ;
#7273=CARTESIAN_POINT ( 'NONE',  ( -1.747541505913277282, 3.837784562140256650, -3.503702292528906526 ) ) ;
#7299=( BOUNDED_SURFACE ( )  B_SPLINE_SURFACE ( 3, 2, ( 
 ( #15103, #13433, #11960 ),
 ( #10480, #3247, #5887 ),
 ( #14900, #17963, #1474 ),
 ( #19346, #1289, #9116 ),
 ( #4318, #16484, #11854 ),
 ( #14699, #13326, #4521 ) ),
 .UNSPECIFIED., .F., .F., .T. ) 
 B_SPLINE_SURFACE_WITH_KNOTS ( ( 4, 2, 4 ),
 ( 3, 3 ),
 ( 0.02032853247518126918, 0.02278863295364821906, 0.02524873343211517240 ),
 ( 0.000000000000000000, 1.000000000000000000 ),
 .UNSPECIFIED. ) 
 GEOMETRIC_REPRESENTATION_ITEM ( )  RATIONAL_B_SPLINE_SURFACE ( (
 ( 1.000000000000000000, 0.8047781615896837382, 1.000000000000000000),
 ( 1.000000000000000000, 0.8123767586289252218, 1.000000000000000000),
 ( 1.000000000000000000, 0.8190662415564388121, 1.000000000000000000),
 ( 1.000000000000000000, 0.8192361015669026303, 1.000000000000000000),
 ( 1.000000000000000000, 0.8126135807103900266, 1.000000000000000000),
 ( 1.000000000000000000, 0.8047712338318593339, 1.000000000000000000) ) ) 
 REPRESENTATION_ITEM ( '' )  SURFACE ( )  );
#7302=EDGE_CURVE ( 'NONE', #19213, #5450, #5336, .T. ) ;
#7363=ADVANCED_FACE ( 'NONE', ( #14939 ), #6773, .T. ) ;
#7369=AXIS2_PLACEMENT_3D ( 'NONE', #7068, #8837, #1390 ) ;
#7383=CIRCLE ( 'NONE', #4263, 2.100000000000000089 ) ;
#7410=VERTEX_POINT ( 'NONE', #2994 ) ;
#7430=CARTESIAN_POINT ( 'NONE',  ( 0.000000000000000000, 0.000000000000000000, -0.3080913168122742518 ) ) ;
#7449=FACE_OUTER_BOUND ( 'NONE', #6876, .T. ) ;
#7471=EDGE_CURVE ( 'NONE', #16922, #5141, #12091, .T. ) ;
#7477=DIRECTION ( 'NONE',  ( -1.000000000000000000, 0.000000000000000000, 0.000000000000000000 ) ) ;
#7503=ORIENTED_EDGE ( 'NONE', *, *, #7011, .F. ) ;
#7541=CYLINDRICAL_SURFACE ( 'NONE', #13496, 2.500000000000000444 ) ;
#7567=CARTESIAN_POINT ( 'NONE',  ( -0.02511973781850462134, 4.877415612947412882, -3.751298745799839462 ) ) ;
#7585=DIRECTION ( 'NONE',  ( 0.000000000000000000, 0.000000000000000000, -1.000000000000000000 ) ) ;
#7599=ORIENTED_EDGE ( 'NONE', *, *, #17561, .F. ) ;
#7611=ORIENTED_EDGE ( 'NONE', *, *, #12720, .F. ) ;
#7616=CARTESIAN_POINT ( 'NONE',  ( 8.673617379884035472E-16, 4.618802153517012954, 0.000000000000000000 ) ) ;
#7620=CARTESIAN_POINT ( 'NONE',  ( -2.000000000000006661, 3.464101615137750834, 0.000000000000000000 ) ) ;
#7622=CARTESIAN_POINT ( 'NONE',  ( -4.197477534772231955, 0.8522413273724368521, -3.505042416683225692 ) ) ;
#7625=ORIENTED_EDGE ( 'NONE', *, *, #3181, .T. ) ;
#7646=CARTESIAN_POINT ( 'NONE',  ( -4.000000000000000000, -1.560351142792950618, -0.2242961665059814425 ) ) ;
#7666=CONICAL_SURFACE ( 'NONE', #4556, 2.059999999999998721, 0.9599310885968738161 ) ;
#7703=CARTESIAN_POINT ( 'NONE',  ( -2.500000000000000888, 0.000000000000000000, -4.974599999999998801 ) ) ;
#7715=ORIENTED_EDGE ( 'NONE', *, *, #2876, .T. ) ;
#7730=DIRECTION ( 'NONE',  ( 1.000000000000000000, 0.000000000000000000, 0.000000000000000000 ) ) ;
#7800=CARTESIAN_POINT ( 'NONE',  ( 3.679171394226031122, 2.494631558665830973, -0.3503314178412474389 ) ) ;
#7810=CARTESIAN_POINT ( 'NONE',  ( 0.000000000000000000, 0.000000000000000000, -5.000000000000000888 ) ) ;
#7824=DIRECTION ( 'NONE',  ( -0.000000000000000000, -0.000000000000000000, 1.000000000000000000 ) ) ;
#7839=ORIENTED_EDGE ( 'NONE', *, *, #14172, .T. ) ;
#7851=CIRCLE ( 'NONE', #15680, 2.499999999999999556 ) ;
#7921=( BOUNDED_SURFACE ( )  B_SPLINE_SURFACE ( 3, 2, ( 
 ( #2360, #8221, #6747 ),
 ( #12731, #18732, #5281 ),
 ( #11252, #17264, #3824 ),
 ( #9786, #8312, #14291 ),
 ( #18839, #17358, #6844 ),
 ( #12833, #5383, #11354 ) ),
 .UNSPECIFIED., .F., .F., .T. ) 
 B_SPLINE_SURFACE_WITH_KNOTS ( ( 4, 2, 4 ),
 ( 3, 3 ),
 ( 0.02027065861071770947, 0.02273072267836921331, 0.02519078674602071716 ),
 ( 0.000000000000000000, 1.000000000000000000 ),
 .UNSPECIFIED. ) 
 GEOMETRIC_REPRESENTATION_ITEM ( )  RATIONAL_B_SPLINE_SURFACE ( (
 ( 1.000000000000000000, 0.8047781708337304885, 1.000000000000000000),
 ( 1.000000000000000000, 0.8123765190705307671, 1.000000000000000000),
 ( 1.000000000000000000, 0.8190656277163975707, 1.000000000000000000),
 ( 1.000000000000000000, 0.8192366903512159348, 1.000000000000000000),
 ( 1.000000000000000000, 0.8126138454302893610, 1.000000000000000000),
 ( 1.000000000000000000, 0.8047712246031417660, 1.000000000000000000) ) ) 
 REPRESENTATION_ITEM ( '' )  SURFACE ( )  );
#7928=VERTEX_POINT ( 'NONE', #4708 ) ;
#7934=CARTESIAN_POINT ( 'NONE',  ( 4.000000000000000000, -2.309401076758514915, -5.000000000000000000 ) ) ;
#7967=CARTESIAN_POINT ( 'NONE',  ( -3.355112389629170799, 2.681727112203152963, -0.2256878752776689534 ) ) ;
#7985=ORIENTED_EDGE ( 'NONE', *, *, #19121, .T. ) ;
#8006=ORIENTED_EDGE ( 'NONE', *, *, #17208, .T. ) ;
#8064=EDGE_CURVE ( 'NONE', #12888, #9683, #19056, .T. ) ;
#8108=AXIS2_PLACEMENT_3D ( 'NONE', #11205, #12685, #6797 ) ;
#8125=ORIENTED_EDGE ( 'NONE', *, *, #5425, .T. ) ;
#8138=CIRCLE ( 'NONE', #10647, 4.000000000000000000 ) ;
#8144=DIRECTION ( 'NONE',  ( -0.000000000000000000, -0.000000000000000000, 1.000000000000000000 ) ) ;
#8151=AXIS2_PLACEMENT_3D ( 'NONE', #2709, #1034, #6997 ) ;
#8154=CIRCLE ( 'NONE', #10665, 4.000000000000000000 ) ;
#8161=CARTESIAN_POINT ( 'NONE',  ( -3.680118525130244400, 2.494084732383327285, -0.3507732604232449702 ) ) ;
#8163=AXIS2_PLACEMENT_3D ( 'NONE', #1466, #287, #6262 ) ;
#8181=AXIS2_PLACEMENT_3D ( 'NONE', #9458, #13868, #9547 ) ;
#8214=CARTESIAN_POINT ( 'NONE',  ( 4.000000000000000000, 0.7924765000094659007, -0.05906175389889852662 ) ) ;
#8221=CARTESIAN_POINT ( 'NONE',  ( 4.000000000000000000, -2.471525695159793035, -3.686886880705770864 ) ) ;
#8225=CARTESIAN_POINT ( 'NONE',  ( -4.000000000000000000, -2.309401076758512694, -3.433295621305382461 ) ) ;
#8240=ADVANCED_FACE ( 'NONE', ( #10162 ), #17542, .F. ) ;
#8263=VERTEX_POINT ( 'NONE', #17734 ) ;
#8272=ORIENTED_EDGE ( 'NONE', *, *, #16352, .T. ) ;
#8287=AXIS2_PLACEMENT_3D ( 'NONE', #14110, #12937, #11162 ) ;
#8312=CARTESIAN_POINT ( 'NONE',  ( 4.000000000000000888, 0.8228435280416209752, -3.430609588141487976 ) ) ;
#8321=ORIENTED_EDGE ( 'NONE', *, *, #16166, .T. ) ;
#8331=DIRECTION ( 'NONE',  ( -1.000000000000000000, 0.000000000000000000, 0.000000000000000000 ) ) ;
#8421=EDGE_CURVE ( 'NONE', #1266, #12888, #3577, .T. ) ;
#8443=CARTESIAN_POINT ( 'NONE',  ( -2.756197834950067094, -3.027510591568735254, -3.223146290109809797 ) ) ;
#8444=LINE ( 'NONE', #14424, #11884 ) ;
#8454=CARTESIAN_POINT ( 'NONE',  ( 2.742827927723449299, 3.035229711104609596, -3.433252694550591233 ) ) ;
#8469=B_SPLINE_CURVE_WITH_KNOTS ( 'NONE', 3,
 ( #5499, #10005, #5601, #13336, #11573 ),
 .UNSPECIFIED., .F., .F.,
 ( 4, 1, 4 ),
 ( 0.000000000000000000, 0.002309401076758505356, 0.004618802153517010713 ),
 .UNSPECIFIED. ) ;
#8505=ORIENTED_EDGE ( 'NONE', *, *, #13232, .F. ) ;
#8525=ORIENTED_EDGE ( 'NONE', *, *, #2604, .T. ) ;
#8540=ADVANCED_FACE ( 'NONE', ( #2032 ), #18609, .T. ) ;
#8563=ADVANCED_FACE ( 'NONE', ( #9464 ), #9000, .T. ) ;
#8584=CARTESIAN_POINT ( 'NONE',  ( -6.259644161404862988E-16, -4.618802153517027165, -3.504271511726793076 ) ) ;
#8588=CARTESIAN_POINT ( 'NONE',  ( -2.682243648011671588, -3.070208061305317759, -0.04852650426602272971 ) ) ;
#8600=FACE_OUTER_BOUND ( 'NONE', #18595, .T. ) ;
#8621=CARTESIAN_POINT ( 'NONE',  ( -5.384454397937118664, 6.702023979852544604E-16, -5.000000000000000000 ) ) ;
#8636=CARTESIAN_POINT ( 'NONE',  ( -2.836893136758495970, -3.208949435745868328, -3.505054077164885484 ) ) ;
#8661=CARTESIAN_POINT ( 'NONE',  ( 4.101954839143060028, 2.368264730582927857, -3.681130640444267854 ) ) ;
#8664=VERTEX_POINT ( 'NONE', #11804 ) ;
#8680=CARTESIAN_POINT ( 'NONE',  ( -1.999999999999999556, 3.464101615137754830, -3.142992957459232795 ) ) ;
#8696=CARTESIAN_POINT ( 'NONE',  ( -2.725741868435985094, 3.045094352034055429, -3.220599429844047012 ) ) ;
#8736=EDGE_CURVE ( 'NONE', #6664, #1514, #11703, .T. ) ;
#8748=CARTESIAN_POINT ( 'NONE',  ( -4.000000000000000000, 2.309401076758498483, -3.433295621305379353 ) ) ;
#8765=DIRECTION ( 'NONE',  ( 1.000000000000000000, 0.000000000000000000, 0.000000000000000000 ) ) ;
#8780=CARTESIAN_POINT ( 'NONE',  ( -3.679171394226034675, -2.494631558665844739, -0.3503314178412558211 ) ) ;
#8786=CARTESIAN_POINT ( 'NONE',  ( -4.000000000000000000, 2.309401076758498483, -3.433295621305379353 ) ) ;
#8805=CIRCLE ( 'NONE', #11301, 2.100000000000000089 ) ;
#8806=EDGE_LOOP ( 'NONE', ( #8321, #8125, #3471, #14290, #16247, #10848, #17066 ) ) ;
#8808=CARTESIAN_POINT ( 'NONE',  ( -0.6448876103708541807, -4.246476118072358474, -0.2256878752776773356 ) ) ;
#8818=ORIENTED_EDGE ( 'NONE', *, *, #9144, .T. ) ;
#8827=CARTESIAN_POINT ( 'NONE',  ( 0.000000000000000000, 0.000000000000000000, 0.000000000000000000 ) ) ;
#8834=DIRECTION ( 'NONE',  ( 0.000000000000000000, 0.000000000000000000, 1.000000000000000000 ) ) ;
#8837=DIRECTION ( 'NONE',  ( 0.000000000000000000, -1.000000000000000000, 0.000000000000000000 ) ) ;
#8875=CARTESIAN_POINT ( 'NONE',  ( -2.344047193898593395, -3.265465875126480455, -1.054683074273691752E-14 ) ) ;
#8908=ORIENTED_EDGE ( 'NONE', *, *, #6096, .F. ) ;
#8909=CARTESIAN_POINT ( 'NONE',  ( 1.144235203016666258, 3.958177651039090250, -0.09382832055445661235 ) ) ;
#8979=FACE_OUTER_BOUND ( 'NONE', #13523, .T. ) ;
#8980=ORIENTED_EDGE ( 'NONE', *, *, #9621, .F. ) ;
#8989=CARTESIAN_POINT ( 'NONE',  ( -4.000000000000000000, -2.472261339043343220, -3.687027428081192326 ) ) ;
#9000=CONICAL_SURFACE ( 'NONE', #551, 4.000000000000000000, 0.8911886515913786111 ) ;
#9001=CARTESIAN_POINT ( 'NONE',  ( 2.499999999999999556, 0.000000000000000000, 3.469446951953614189E-15 ) ) ;
#9002=ORIENTED_EDGE ( 'NONE', *, *, #16166, .F. ) ;
#9015=CARTESIAN_POINT ( 'NONE',  ( -4.198928548860774157, 0.8158838809860065044, -3.526471437616918170 ) ) ;
#9072=CARTESIAN_POINT ( 'NONE',  ( 2.500000000000000444, 0.000000000000000000, -5.000000000000000888 ) ) ;
#9082=CARTESIAN_POINT ( 'NONE',  ( 4.000000000000000000, 0.000000000000000000, 0.000000000000000000 ) ) ;
#9084=VECTOR ( 'NONE', #9455, 1000.000000000000000 ) ;
#9086=CARTESIAN_POINT ( 'NONE',  ( 2.500000000000000888, 3.061616997868384127E-16, -4.974599999999998801 ) ) ;
#9093=ORIENTED_EDGE ( 'NONE', *, *, #17571, .F. ) ;
#9116=CARTESIAN_POINT ( 'NONE',  ( 2.807080416178989513, -3.225969019225150003, -3.502507215260505014 ) ) ;
#9117=TOROIDAL_SURFACE ( 'NONE', #18849, 5.384454397937118664, 0.5155456020628804703 ) ;
#9144=EDGE_CURVE ( 'NONE', #162, #18909, #8469, .T. ) ;
#9145=CARTESIAN_POINT ( 'NONE',  ( 4.203833317240879275, 1.627343821129582979, -3.597273115243889929 ) ) ;
#9163=CARTESIAN_POINT ( 'NONE',  ( 2.805705207896068476, -3.226868319750173075, -3.503898532754370354 ) ) ;
#9165=ORIENTED_EDGE ( 'NONE', *, *, #9540, .F. ) ;
#9169=ADVANCED_FACE ( 'NONE', ( #9902 ), #10038, .F. ) ;
#9179=ORIENTED_EDGE ( 'NONE', *, *, #7013, .T. ) ;
#9183=DIRECTION ( 'NONE',  ( 1.000000000000000000, 0.000000000000000000, 0.000000000000000000 ) ) ;
#9202=EDGE_CURVE ( 'NONE', #5017, #10265, #10796, .T. ) ;
#9206=DIRECTION ( 'NONE',  ( -0.000000000000000000, -0.000000000000000000, 1.000000000000000000 ) ) ;
#9235=DIRECTION ( 'NONE',  ( 0.000000000000000000, 0.000000000000000000, 1.000000000000000000 ) ) ;
#9246=CARTESIAN_POINT ( 'NONE',  ( -4.197393957002303999, -0.8151795401431414234, -3.503767560748935139 ) ) ;
#9250=EDGE_LOOP ( 'NONE', ( #1830, #6501, #13589, #11948 ) ) ;
#9335=FACE_OUTER_BOUND ( 'NONE', #3766, .T. ) ;
#9352=DIRECTION ( 'NONE',  ( 1.000000000000000000, 0.000000000000000000, 0.000000000000000000 ) ) ;
#9355=CARTESIAN_POINT ( 'NONE',  ( 1.734723475976807094E-15, 4.618802153517012954, -0.4999999999999995559 ) ) ;
#9361=CARTESIAN_POINT ( 'NONE',  ( 3.999999999999999112, -0.3979232138631231819, -5.929230630780099908E-17 ) ) ;
#9408=DIRECTION ( 'NONE',  ( -0.000000000000000000, 0.000000000000000000, -1.000000000000000000 ) ) ;
#9429=DIRECTION ( 'NONE',  ( 0.000000000000000000, 0.000000000000000000, 1.000000000000000000 ) ) ;
#9444=CIRCLE ( 'NONE', #16679, 5.384454397937118664 ) ;
#9451=B_SPLINE_CURVE_WITH_KNOTS ( 'NONE', 3,
 ( #12114, #13682, #17958, #1832, #7800, #18315 ),
 .UNSPECIFIED., .F., .F.,
 ( 4, 2, 4 ),
 ( 0.002365888236227995517, 0.003551327329835084114, 0.004736766423442172712 ),
 .UNSPECIFIED. ) ;
#9455=DIRECTION ( 'NONE',  ( 0.000000000000000000, 0.000000000000000000, 1.000000000000000000 ) ) ;
#9458=CARTESIAN_POINT ( 'NONE',  ( 0.000000000000000000, 0.000000000000000000, -4.974599999999998801 ) ) ;
#9464=FACE_OUTER_BOUND ( 'NONE', #10274, .T. ) ;
#9477=EDGE_LOOP ( 'NONE', ( #1145, #5206, #9002, #16637, #11288 ) ) ;
#9498=EDGE_CURVE ( 'NONE', #10423, #6664, #15731, .T. ) ;
#9505=LINE ( 'NONE', #16788, #19375 ) ;
#9518=ORIENTED_EDGE ( 'NONE', *, *, #10216, .T. ) ;
#9524=CARTESIAN_POINT ( 'NONE',  ( 4.000000000000000000, 2.309401076758497151, -5.000000000000000000 ) ) ;
#9529=CARTESIAN_POINT ( 'NONE',  ( 4.101954839143059139, -2.368264730582948285, -3.681130640444269631 ) ) ;
#9540=EDGE_CURVE ( 'NONE', #14765, #1266, #3626, .T. ) ;
#9547=DIRECTION ( 'NONE',  ( -1.000000000000000000, 0.000000000000000000, 0.000000000000000000 ) ) ;
#9559=CARTESIAN_POINT ( 'NONE',  ( -4.000000000000000000, -1.942223658245633811, -0.3516579909967644246 ) ) ;
#9604=ADVANCED_FACE ( 'NONE', ( #2664 ), #12067, .T. ) ;
#9621=EDGE_CURVE ( 'NONE', #10976, #13559, #7383, .T. ) ;
#9624=CARTESIAN_POINT ( 'NONE',  ( -2.000000000000007550, -3.464101615137749945, 0.000000000000000000 ) ) ;
#9640=AXIS2_PLACEMENT_3D ( 'NONE', #5874, #93, #13607 ) ;
#9642=VECTOR ( 'NONE', #6948, 1000.000000000000114 ) ;
#9655=CARTESIAN_POINT ( 'NONE',  ( 4.211140560182196957, 2.431303136016536470, -3.745885042887433514 ) ) ;
#9683=VERTEX_POINT ( 'NONE', #12836 ) ;
#9695=CARTESIAN_POINT ( 'NONE',  ( -2.807080416178626692, 3.225969019225154444, -3.502507215260441065 ) ) ;
#9744=CARTESIAN_POINT ( 'NONE',  ( -1.317756351988340180, 3.857995168970202116, -0.04852650426601388955 ) ) ;
#9759=CARTESIAN_POINT ( 'NONE',  ( 3.861362476283255685, 2.629030857715988656, -3.671615880910370500 ) ) ;
#9774=VERTEX_POINT ( 'NONE', #9001 ) ;
#9786=CARTESIAN_POINT ( 'NONE',  ( 4.000000000000000000, 0.8378280264232961239, -3.220590601395640018 ) ) ;
#9795=DIRECTION ( 'NONE',  ( -1.000000000000000000, 0.000000000000000000, 0.000000000000000000 ) ) ;
#9796=FACE_OUTER_BOUND ( 'NONE', #2464, .T. ) ;
#9851=( NAMED_UNIT ( * ) SI_UNIT ( $, .STERADIAN. ) SOLID_ANGLE_UNIT ( ) );
#9855=B_SPLINE_CURVE_WITH_KNOTS ( 'NONE', 3,
 ( #2844, #17946, #8808, #14782, #4504, #17842, #4480, #4402 ),
 .UNSPECIFIED., .F., .F.,
 ( 4, 2, 2, 4 ),
 ( 2.465131517390770070E-07, 0.001183067374689869946, 0.001774477805458935659, 0.002365888236228001588 ),
 .UNSPECIFIED. ) ;
#9857=EDGE_CURVE ( 'NONE', #848, #6664, #17244, .T. ) ;
#9885=DIRECTION ( 'NONE',  ( -0.000000000000000000, -0.000000000000000000, 1.000000000000000000 ) ) ;
#9902=FACE_OUTER_BOUND ( 'NONE', #9250, .T. ) ;
#9914=CARTESIAN_POINT ( 'NONE',  ( 4.140404888673277384, 2.228338276487440428, -3.686887068327033390 ) ) ;
#9927=FACE_OUTER_BOUND ( 'NONE', #17723, .T. ) ;
#9931=FACE_OUTER_BOUND ( 'NONE', #14149, .T. ) ;
#9947=ORIENTED_EDGE ( 'NONE', *, *, #18277, .F. ) ;
#9960=ORIENTED_EDGE ( 'NONE', *, *, #8736, .T. ) ;
#9973=CARTESIAN_POINT ( 'NONE',  ( -2.500000000000000888, 0.000000000000000000, -4.974599999999998801 ) ) ;
#9983=ORIENTED_EDGE ( 'NONE', *, *, #16132, .T. ) ;
#10005=CARTESIAN_POINT ( 'NONE',  ( 3.333333333333332593, 2.694301256218250007, -3.300726591567078483 ) ) ;
#10014=CARTESIAN_POINT ( 'NONE',  ( 3.453038570460273071, 2.625189405340834448, -3.535263753543585352 ) ) ;
#10038=( BOUNDED_SURFACE ( )  B_SPLINE_SURFACE ( 3, 2, ( 
 ( #16101, #19359, #11674 ),
 ( #1098, #2684, #5896 ),
 ( #8443, #7271, #8636 ),
 ( #14608, #14711, #14513 ),
 ( #16194, #13149, #17481 ),
 ( #4328, #4230, #16006 ) ),
 .UNSPECIFIED., .F., .F., .F. ) 
 B_SPLINE_SURFACE_WITH_KNOTS ( ( 4, 2, 4 ),
 ( 3, 3 ),
 ( 0.02032853247518126918, 0.02278863295364821906, 0.02524873343211516893 ),
 ( 0.000000000000000000, 1.000000000000000000 ),
 .UNSPECIFIED. ) 
 GEOMETRIC_REPRESENTATION_ITEM ( )  RATIONAL_B_SPLINE_SURFACE ( (
 ( 1.000000000000000000, 0.8047781615896838492, 1.000000000000000000),
 ( 1.000000000000000000, 0.8123767586288186404, 1.000000000000000000),
 ( 1.000000000000000000, 0.8190662415565814758, 1.000000000000000000),
 ( 1.000000000000000000, 0.8192361015667604107, 1.000000000000000000),
 ( 1.000000000000000000, 0.8126135807104967190, 1.000000000000000000),
 ( 1.000000000000000000, 0.8047712338318580017, 1.000000000000000000) ) ) 
 REPRESENTATION_ITEM ( '' )  SURFACE ( )  );
#10041=CARTESIAN_POINT ( 'NONE',  ( 0.000000000000000000, 0.000000000000000000, -4.484454397937119197 ) ) ;
#10050=CARTESIAN_POINT ( 'NONE',  ( 2.449848172108560096, 3.432307619358740514, -3.503702292528905637 ) ) ;
#10062=DIRECTION ( 'NONE',  ( 0.000000000000000000, 0.000000000000000000, 1.000000000000000000 ) ) ;
#10066=CARTESIAN_POINT ( 'NONE',  ( 4.197393957002303999, 7.772902908466098641E-14, -3.503767560748929810 ) ) ;
#10078=EDGE_LOOP ( 'NONE', ( #12793, #10911, #10539, #5342 ) ) ;
#10088=ORIENTED_EDGE ( 'NONE', *, *, #2710, .F. ) ;
#10115=CARTESIAN_POINT ( 'NONE',  ( 4.235886605889389145, 2.417314728048528760, -3.751161874094018245 ) ) ;
#10162=FACE_OUTER_BOUND ( 'NONE', #13127, .T. ) ;
#10168=ADVANCED_FACE ( 'NONE', ( #7027 ), #15959, .F. ) ;
#10181=DIRECTION ( 'NONE',  ( -1.000000000000000000, 0.000000000000000000, 0.000000000000000000 ) ) ;
#10192=ORIENTED_EDGE ( 'NONE', *, *, #6163, .F. ) ;
#10201=CARTESIAN_POINT ( 'NONE',  ( 1.274258131564866448, 3.883108878240963513, -3.220599429844046568 ) ) ;
#10216=EDGE_CURVE ( 'NONE', #19213, #7928, #4187, .T. ) ;
#10222=EDGE_CURVE ( 'NONE', #1748, #12905, #5653, .T. ) ;
#10255=CARTESIAN_POINT ( 'NONE',  ( -3.436319922987618902, 2.634841920961291439, -3.531542292955721862 ) ) ;
#10265=VERTEX_POINT ( 'NONE', #11819 ) ;
#10274=EDGE_LOOP ( 'NONE', ( #12319, #9947, #18599 ) ) ;
#10324=DIRECTION ( 'NONE',  ( -0.000000000000000000, -0.000000000000000000, 1.000000000000000000 ) ) ;
#10359=AXIS2_PLACEMENT_3D ( 'NONE', #2871, #8834, #16191 ) ;
#10365=CARTESIAN_POINT ( 'NONE',  ( -4.203934362469166963, -1.640673743454851286, -3.598432614606932756 ) ) ;
#10380=CARTESIAN_POINT ( 'NONE',  ( 1.734723475976807094E-15, 4.618802153517012954, -0.4999999999999995559 ) ) ;
#10392=CARTESIAN_POINT ( 'NONE',  ( -4.000000000000000000, 2.309401076758498483, -0.4999999999999927280 ) ) ;
#10393=CARTESIAN_POINT ( 'NONE',  ( -4.197393957002303999, -7.773935952363655451E-14, -3.503767560748929810 ) ) ;
#10422=PRODUCT_DEFINITION_FORMATION_WITH_SPECIFIED_SOURCE ( 'ANY', '', #6944, .NOT_KNOWN. ) ;
#10423=VERTEX_POINT ( 'NONE', #8786 ) ;
#10433=ORIENTED_EDGE ( 'NONE', *, *, #2710, .T. ) ;
#10436=EDGE_LOOP ( 'NONE', ( #16127, #15628, #1999 ) ) ;
#10471=EDGE_CURVE ( 'NONE', #10265, #7928, #6573, .T. ) ;
#10472=CARTESIAN_POINT ( 'NONE',  ( 4.000000000000000000, 2.309401076758497151, -5.000000000000000000 ) ) ;
#10480=CARTESIAN_POINT ( 'NONE',  ( 0.5276280594147412240, -4.314175951381924889, -3.320322319201654881 ) ) ;
#10493=VECTOR ( 'NONE', #17269, 1000.000000000000000 ) ;
#10499=CARTESIAN_POINT ( 'NONE',  ( -4.211140560182196957, 2.431303136016537803, -3.745885042887433514 ) ) ;
#10517=DIRECTION ( 'NONE',  ( -1.000000000000000000, 0.000000000000000000, 0.000000000000000000 ) ) ;
#10527=ORIENTED_EDGE ( 'NONE', *, *, #17561, .T. ) ;
#10539=ORIENTED_EDGE ( 'NONE', *, *, #16114, .T. ) ;
#10570=PRODUCT_DEFINITION ( 'UNKNOWN', '', #10422, #19144 ) ;
#10575=DIRECTION ( 'NONE',  ( -0.000000000000000000, 0.000000000000000000, -1.000000000000000000 ) ) ;
#10580=CARTESIAN_POINT ( 'NONE',  ( -4.197393957002303999, 0.4069871074557429025, -3.503767560748926257 ) ) ;
#10609=VERTEX_POINT ( 'NONE', #13864 ) ;
#10624=CARTESIAN_POINT ( 'NONE',  ( -6.473970235329672780E-16, -4.862606272033106691, -3.745885042887442395 ) ) ;
#10627=ORIENTED_EDGE ( 'NONE', *, *, #9498, .T. ) ;
#10632=EDGE_CURVE ( 'NONE', #13559, #1748, #3490, .T. ) ;
#10646=FACE_OUTER_BOUND ( 'NONE', #15803, .T. ) ;
#10647=AXIS2_PLACEMENT_3D ( 'NONE', #8827, #10575, #16681 ) ;
#10651=AXIS2_PLACEMENT_3D ( 'NONE', #14165, #4177, #5539 ) ;
#10665=AXIS2_PLACEMENT_3D ( 'NONE', #16118, #11780, #7477 ) ;
#10670=UNCERTAINTY_MEASURE_WITH_UNIT (LENGTH_MEASURE( 1.000000000000000082E-05 ), #12129, 'distance_accuracy_value', 'NONE');
#10709=CARTESIAN_POINT ( 'NONE',  ( 1.411581201560190495E-15, 4.862606272033091592, -3.745885042887436622 ) ) ;
#10723=CARTESIAN_POINT ( 'NONE',  ( 4.211140560182196957, -2.431303136016555122, -3.745885042887436622 ) ) ;
#10724=FACE_OUTER_BOUND ( 'NONE', #7228, .T. ) ;
#10737=CARTESIAN_POINT ( 'NONE',  ( 0.000000000000000000, 0.000000000000000000, -4.484454397937119197 ) ) ;
#10751=VERTEX_POINT ( 'NONE', #2416 ) ;
#10768=ADVANCED_FACE ( 'NONE', ( #9931 ), #12554, .F. ) ;
#10774=EDGE_CURVE ( 'NONE', #162, #10751, #147, .T. ) ;
#10786=CARTESIAN_POINT ( 'NONE',  ( -3.510273485745307287, -2.827716139362669967, -3.610536846335890004 ) ) ;
#10796=CIRCLE ( 'NONE', #7369, 0.5155456020628804703 ) ;
#10797=CARTESIAN_POINT ( 'NONE',  ( 2.548804901056335857E-15, 4.736522675502163437, -3.681124513963624612 ) ) ;
#10834=CARTESIAN_POINT ( 'NONE',  ( 0.000000000000000000, 0.000000000000000000, -0.3080913168122742518 ) ) ;
#10839=CARTESIAN_POINT ( 'NONE',  ( -2.688821387764050996E-14, -4.618802153517012954, -0.4999999999999995559 ) ) ;
#10848=ORIENTED_EDGE ( 'NONE', *, *, #17927, .T. ) ;
#10852=CARTESIAN_POINT ( 'NONE',  ( 0.000000000000000000, 0.000000000000000000, -0.2800830152838844622 ) ) ;
#10862=CARTESIAN_POINT ( 'NONE',  ( 0.000000000000000000, 0.000000000000000000, -4.974599999999998801 ) ) ;
#10867=CARTESIAN_POINT ( 'NONE',  ( 0.000000000000000000, 0.000000000000000000, 0.000000000000000000 ) ) ;
#10899=B_SPLINE_CURVE_WITH_KNOTS ( 'NONE', 3,
 ( #1498, #11775, #12171, #6016, #19371 ),
 .UNSPECIFIED., .F., .F.,
 ( 4, 1, 4 ),
 ( 0.000000000000000000, 0.002309401076758505790, 0.004618802153517011580 ),
 .UNSPECIFIED. ) ;
#10911=ORIENTED_EDGE ( 'NONE', *, *, #6636, .F. ) ;
#10942=( LENGTH_UNIT ( ) NAMED_UNIT ( * ) SI_UNIT ( .MILLI., .METRE. ) );
#10976=VERTEX_POINT ( 'NONE', #1706 ) ;
#10986=DIRECTION ( 'NONE',  ( 0.000000000000000000, 0.000000000000000000, 1.000000000000000000 ) ) ;
#10994=VECTOR ( 'NONE', #10986, 1000.000000000000000 ) ;
#11007=CARTESIAN_POINT ( 'NONE',  ( -2.687328764639638656, 3.067272167851286202, -0.05923475698270370959 ) ) ;
#11021=ORIENTED_EDGE ( 'NONE', *, *, #16666, .F. ) ;
#11038=FILL_AREA_STYLE_COLOUR ( '', #14038 ) ;
#11045=ADVANCED_BREP_SHAPE_REPRESENTATION ( '', ( #2292, #10359 ), #11543 ) ;
#11108=CARTESIAN_POINT ( 'NONE',  ( -4.000000000000000000, 1.941961291383472732, -0.3515519931180205448 ) ) ;
#11149=ORIENTED_EDGE ( 'NONE', *, *, #16132, .F. ) ;
#11162=DIRECTION ( 'NONE',  ( -1.000000000000000000, 0.000000000000000000, 0.000000000000000000 ) ) ;
#11164=EDGE_CURVE ( 'NONE', #1748, #71, #8805, .T. ) ;
#11205=CARTESIAN_POINT ( 'NONE',  ( 1.567478505476134606E-15, 4.618802153517012066, -5.000000000000000000 ) ) ;
#11229=VERTEX_POINT ( 'NONE', #10066 ) ;
#11252=CARTESIAN_POINT ( 'NONE',  ( 4.000000000000000000, -0.8732470631449981147, -3.223155494240760088 ) ) ;
#11263=CARTESIAN_POINT ( 'NONE',  ( 3.333333333333335702, -2.694301256218268215, -3.300726591567084256 ) ) ;
#11288=ORIENTED_EDGE ( 'NONE', *, *, #5329, .F. ) ;
#11294=CARTESIAN_POINT ( 'NONE',  ( -2.345747346278108214, 3.264484291692489215, -0.01223254789873409049 ) ) ;
#11301=AXIS2_PLACEMENT_3D ( 'NONE', #10852, #16861, #3420 ) ;
#11318=CARTESIAN_POINT ( 'NONE',  ( 2.345747346278113987, -3.264484291692503870, -0.01223254789874484924 ) ) ;
#11330=ORIENTED_EDGE ( 'NONE', *, *, #2876, .F. ) ;
#11337=ORIENTED_EDGE ( 'NONE', *, *, #18145, .T. ) ;
#11354=CARTESIAN_POINT ( 'NONE',  ( 4.211405965630455661, 2.460463115436283932, -3.751298928144577882 ) ) ;
#11380=CARTESIAN_POINT ( 'NONE',  ( -4.211140560182196957, 2.431303136016537803, -3.745885042887433514 ) ) ;
#11382=ORIENTED_EDGE ( 'NONE', *, *, #2943, .T. ) ;
#11399=ORIENTED_EDGE ( 'NONE', *, *, #17483, .F. ) ;
#11435=ADVANCED_FACE ( 'NONE', ( #8979 ), #9117, .T. ) ;
#11490=ORIENTED_EDGE ( 'NONE', *, *, #12182, .F. ) ;
#11496=CARTESIAN_POINT ( 'NONE',  ( -4.000000000000000000, 0.1981133338132459731, 2.096406544454392723E-17 ) ) ;
#11503=VECTOR ( 'NONE', #5508, 1000.000000000000000 ) ;
#11505=CARTESIAN_POINT ( 'NONE',  ( 3.355112389629172576, -2.681727112203168950, -0.2256878752776777242 ) ) ;
#11543=( GEOMETRIC_REPRESENTATION_CONTEXT ( 3 ) GLOBAL_UNCERTAINTY_ASSIGNED_CONTEXT ( ( #10670 ) ) GLOBAL_UNIT_ASSIGNED_CONTEXT ( ( #12129, #2245, #9851 ) ) REPRESENTATION_CONTEXT ( 'NONE', 'WORKASPACE' ) );
#11565=B_SPLINE_CURVE_WITH_KNOTS ( 'NONE', 3,
 ( #10709, #6114, #10797, #16614, #12085, #13560 ),
 .UNSPECIFIED., .F., .F.,
 ( 4, 2, 4 ),
 ( -3.640115492407174633E-06, 0.0002066546034006553863, 0.0004169493222937179812 ),
 .UNSPECIFIED. ) ;
#11567=EDGE_CURVE ( 'NONE', #1014, #4790, #16717, .T. ) ;
#11573=CARTESIAN_POINT ( 'NONE',  ( 1.567478505476134606E-15, 4.618802153517012066, -3.433295621305382905 ) ) ;
#11583=ADVANCED_FACE ( 'NONE', ( #2222 ), #11613, .F. ) ;
#11613=CONICAL_SURFACE ( 'NONE', #8181, 2.500000000000000888, 0.9599310885968785900 ) ;
#11628=CARTESIAN_POINT ( 'NONE',  ( -2.059999999999998721, 2.522772406243545965E-16, -0.3080913168122742518 ) ) ;
#11634=CARTESIAN_POINT ( 'NONE',  ( -1.243802165048909503, 3.900692638707381921, -3.223146290109805800 ) ) ;
#11642=EDGE_LOOP ( 'NONE', ( #1722, #8980, #9983, #15779 ) ) ;
#11654=DIRECTION ( 'NONE',  ( -0.000000000000000000, -0.000000000000000000, 1.000000000000000000 ) ) ;
#11674=CARTESIAN_POINT ( 'NONE',  ( -4.235886605889389145, -2.417314728048544303, -3.751161874094020909 ) ) ;
#11703=LINE ( 'NONE', #15941, #6816 ) ;
#11728=DIRECTION ( 'NONE',  ( -0.000000000000000000, -0.000000000000000000, 1.000000000000000000 ) ) ;
#11733=CARTESIAN_POINT ( 'NONE',  ( -4.204114297095464359, 1.660363174096617156, -3.602136431857887011 ) ) ;
#11772=B_SPLINE_CURVE_WITH_KNOTS ( 'NONE', 3,
 ( #2321, #12896, #11505, #1128, #2624, #11318, #938, #1041 ),
 .UNSPECIFIED., .F., .F.,
 ( 4, 2, 2, 4 ),
 ( 2.465131517071610173E-07, 0.001183067374689837636, 0.001774477805458902699, 0.002365888236227967761 ),
 .UNSPECIFIED. ) ;
#11774=EDGE_CURVE ( 'NONE', #5017, #442, #1169, .T. ) ;
#11775=CARTESIAN_POINT ( 'NONE',  ( 3.999999999999999112, -1.539600717839012978, -3.300726591567080703 ) ) ;
#11780=DIRECTION ( 'NONE',  ( -0.000000000000000000, 0.000000000000000000, -1.000000000000000000 ) ) ;
#11804=CARTESIAN_POINT ( 'NONE',  ( -6.259644161404860030E-16, -4.618802153517027165, -3.433295621305388234 ) ) ;
#11816=FACE_OUTER_BOUND ( 'NONE', #11642, .T. ) ;
#11819=CARTESIAN_POINT ( 'NONE',  ( 5.560781378645575757, 0.000000000000000000, -4.000000000000000000 ) ) ;
#11832=CARTESIAN_POINT ( 'NONE',  ( -4.000000000000000000, 2.511478553582031203, -3.469254451724764543 ) ) ;
#11843=CARTESIAN_POINT ( 'NONE',  ( -4.101948962585905356, -2.368261337751088824, -3.681124513963624167 ) ) ;
#11846=CIRCLE ( 'NONE', #4022, 4.000000000000000000 ) ;
#11854=CARTESIAN_POINT ( 'NONE',  ( 3.522875095019493141, -2.820352903225631369, -3.598441714920572299 ) ) ;
#11884=VECTOR ( 'NONE', #1008, 999.9999999999998863 ) ;
#11925=CARTESIAN_POINT ( 'NONE',  ( 4.000000000000000000, 2.309401076758497151, -5.000000000000000000 ) ) ;
#11928=FACE_BOUND ( 'NONE', #13674, .T. ) ;
#11933=( NAMED_UNIT ( * ) SI_UNIT ( $, .STERADIAN. ) SOLID_ANGLE_UNIT ( ) );
#11948=ORIENTED_EDGE ( 'NONE', *, *, #18145, .F. ) ;
#11956=EDGE_CURVE ( 'NONE', #14141, #2509, #5484, .T. ) ;
#11960=CARTESIAN_POINT ( 'NONE',  ( -0.02448733951239248641, -4.877042772274742255, -3.751161874094027571 ) ) ;
#11992=ORIENTED_EDGE ( 'NONE', *, *, #6163, .T. ) ;
#11993=CARTESIAN_POINT ( 'NONE',  ( 1.655952806101427033, -3.662737355149048302, -1.182683869819604841E-14 ) ) ;
#12034=APPLICATION_CONTEXT ( 'automotive_design' ) ;
#12048=FACE_OUTER_BOUND ( 'NONE', #7025, .T. ) ;
#12067=CONICAL_SURFACE ( 'NONE', #13636, 4.000000000000000000, 0.8911886515913786111 ) ;
#12085=CARTESIAN_POINT ( 'NONE',  ( 1.567478505476135000E-15, 4.618802153517012954, -3.504269196027527844 ) ) ;
#12091=LINE ( 'NONE', #16521, #2093 ) ;
#12114=CARTESIAN_POINT ( 'NONE',  ( 2.000000000000008882, 3.464101615137749945, 0.000000000000000000 ) ) ;
#12120=CARTESIAN_POINT ( 'NONE',  ( -2.171643655288372443, 3.365003104552320767, 2.541098841762897165E-18 ) ) ;
#12129=( LENGTH_UNIT ( ) NAMED_UNIT ( * ) SI_UNIT ( .MILLI., .METRE. ) );
#12152=CARTESIAN_POINT ( 'NONE',  ( -4.000000000000000000, 0.000000000000000000, 0.000000000000000000 ) ) ;
#12169=ADVANCED_FACE ( 'NONE', ( #3557 ), #12285, .T. ) ;
#12171=CARTESIAN_POINT ( 'NONE',  ( 4.000000000000000000, -1.084202172485504434E-14, -3.142992957459231906 ) ) ;
#12173=DIRECTION ( 'NONE',  ( -0.000000000000000000, -0.000000000000000000, 1.000000000000000000 ) ) ;
#12182=EDGE_CURVE ( 'NONE', #10423, #18115, #6685, .T. ) ;
#12196=CARTESIAN_POINT ( 'NONE',  ( 1.747541505913279281, -3.837784562140273081, -3.503702292528912299 ) ) ;
#12263=EDGE_CURVE ( 'NONE', #11229, #10609, #16022, .T. ) ;
#12285=PLANE ( 'NONE',  #4912 ) ;
#12319=ORIENTED_EDGE ( 'NONE', *, *, #13232, .T. ) ;
#12343=DIRECTION ( 'NONE',  ( -0.000000000000000000, 0.000000000000000000, -1.000000000000000000 ) ) ;
#12356=CARTESIAN_POINT ( 'NONE',  ( -3.861362476283256129, -2.629030857716004199, -3.671615880910374941 ) ) ;
#12362=CARTESIAN_POINT ( 'NONE',  ( 0.000000000000000000, 0.000000000000000000, -4.694516984716113228 ) ) ;
#12400=CARTESIAN_POINT ( 'NONE',  ( -0.3208286057739654917, 4.433571671609680465, -0.3503314178412548774 ) ) ;
#12438=DIRECTION ( 'NONE',  ( -1.000000000000000000, 0.000000000000000000, 0.000000000000000000 ) ) ;
#12447=FACE_OUTER_BOUND ( 'NONE', #12479, .T. ) ;
#12478=CARTESIAN_POINT ( 'NONE',  ( -4.000000000000000000, 2.309401076758498483, -5.000000000000000000 ) ) ;
#12479=EDGE_LOOP ( 'NONE', ( #5043, #16418, #5680 ) ) ;
#12515=SURFACE_STYLE_FILL_AREA ( #14368 ) ;
#12537=CIRCLE ( 'NONE', #5976, 5.560781378645573980 ) ;
#12544=CIRCLE ( 'NONE', #3776, 2.499999999999999556 ) ;
#12554=CONICAL_SURFACE ( 'NONE', #8151, 2.500000000000000888, 0.9599310885968785900 ) ;
#12586=PLANE ( 'NONE',  #8108 ) ;
#12647=CARTESIAN_POINT ( 'NONE',  ( 0.000000000000000000, 0.000000000000000000, -4.000000000000000000 ) ) ;
#12684=ORIENTED_EDGE ( 'NONE', *, *, #10222, .F. ) ;
#12685=DIRECTION ( 'NONE',  ( -0.5000000000000016653, 0.8660254037844378194, 0.000000000000000000 ) ) ;
#12699=DIRECTION ( 'NONE',  ( 0.8660254037844379305, 0.5000000000000013323, 0.000000000000000000 ) ) ;
#12720=EDGE_CURVE ( 'NONE', #13559, #10976, #15577, .T. ) ;
#12731=CARTESIAN_POINT ( 'NONE',  ( 4.000000000000000000, -1.700175430507292473, -3.320327275037661785 ) ) ;
#12759=ORIENTED_EDGE ( 'NONE', *, *, #2604, .F. ) ;
#12767=CARTESIAN_POINT ( 'NONE',  ( 4.197393957002303999, -0.4069871074557456780, -3.503767560748925813 ) ) ;
#12793=ORIENTED_EDGE ( 'NONE', *, *, #10774, .T. ) ;
#12795=DIRECTION ( 'NONE',  ( -0.000000000000000000, -0.000000000000000000, 1.000000000000000000 ) ) ;
#12833=CARTESIAN_POINT ( 'NONE',  ( 4.000000000000000000, 2.512223110932545023, -3.469391141908803711 ) ) ;
#12836=CARTESIAN_POINT ( 'NONE',  ( 4.000000000000000000, 2.309401076758515803, -0.4999999999999995559 ) ) ;
#12888=VERTEX_POINT ( 'NONE', #13145 ) ;
#12896=CARTESIAN_POINT ( 'NONE',  ( 3.680118525130245732, -2.494084732383344605, -0.3507732604232533524 ) ) ;
#12905=VERTEX_POINT ( 'NONE', #894 ) ;
#12937=DIRECTION ( 'NONE',  ( 0.000000000000000000, 0.000000000000000000, -1.000000000000000000 ) ) ;
#12959=CARTESIAN_POINT ( 'NONE',  ( 0.5636800770130377947, 4.293361309317166530, -3.531542292954102713 ) ) ;
#12976=CARTESIAN_POINT ( 'NONE',  ( 4.024499207728657879, 2.323545700935571556, -3.572172305156506411 ) ) ;
#12982=AXIS2_PLACEMENT_3D ( 'NONE', #15099, #13430, #10181 ) ;
#12994=B_SPLINE_CURVE_WITH_KNOTS ( 'NONE', 3,
 ( #15699, #2278, #7055, #11263, #13038 ),
 .UNSPECIFIED., .F., .F.,
 ( 4, 1, 4 ),
 ( 5.640274452250024914E-20, 0.002309401076758505356, 0.004618802153517010713 ),
 .UNSPECIFIED. ) ;
#12997=CONICAL_SURFACE ( 'NONE', #8287, 4.000000000000000000, 0.8911886515913786111 ) ;
#13008=CARTESIAN_POINT ( 'NONE',  ( -5.560781378645573980, 0.000000000000000000, -4.000000000000000000 ) ) ;
#13015=CARTESIAN_POINT ( 'NONE',  ( 0.000000000000000000, 0.000000000000000000, -25.03750572909317285 ) ) ;
#13038=CARTESIAN_POINT ( 'NONE',  ( 4.000000000000000000, -2.309401076758514915, -3.433295621305383349 ) ) ;
#13065=CARTESIAN_POINT ( 'NONE',  ( -4.211140560182196957, 2.431303136016537803, -3.745885042887433514 ) ) ;
#13096=ORIENTED_EDGE ( 'NONE', *, *, #17927, .F. ) ;
#13109=CARTESIAN_POINT ( 'NONE',  ( -1.257172072275743346, 3.892973519171203378, -3.433252694550776862 ) ) ;
#13127=EDGE_LOOP ( 'NONE', ( #568, #13467, #14179, #13969 ) ) ;
#13145=CARTESIAN_POINT ( 'NONE',  ( 4.000000000000000000, 0.000000000000000000, 0.000000000000000000 ) ) ;
#13149=CARTESIAN_POINT ( 'NONE',  ( -0.5636800770129166693, -4.293361309317430319, -3.531542292955206275 ) ) ;
#13152=CARTESIAN_POINT ( 'NONE',  ( -0.3461262719736137305, 4.658553426539289610, -3.671615880910373608 ) ) ;
#13158=CARTESIAN_POINT ( 'NONE',  ( 2.836893136758676270, 3.208949435745843903, -3.505054077164911241 ) ) ;
#13201=DIRECTION ( 'NONE',  ( -0.8191520442889875797, 1.003171929053519570E-16, 0.5735764363510522656 ) ) ;
#13222=DIRECTION ( 'NONE',  ( -1.000000000000000000, 0.000000000000000000, 0.000000000000000000 ) ) ;
#13232=EDGE_CURVE ( 'NONE', #5072, #8263, #14335, .T. ) ;
#13268=ORIENTED_EDGE ( 'NONE', *, *, #13395, .T. ) ;
#13289=ORIENTED_EDGE ( 'NONE', *, *, #8064, .F. ) ;
#13305=FACE_OUTER_BOUND ( 'NONE', #17533, .T. ) ;
#13307=CARTESIAN_POINT ( 'NONE',  ( -4.000000000000000000, 2.471528634177585282, -3.686887442155186712 ) ) ;
#13318=EDGE_LOOP ( 'NONE', ( #4208, #10433, #2185, #3852 ) ) ;
#13326=CARTESIAN_POINT ( 'NONE',  ( 4.141042297810615835, -2.227970268150433863, -3.687027686973623819 ) ) ;
#13336=CARTESIAN_POINT ( 'NONE',  ( 0.6666666666666689611, 4.233901974057261874, -3.300726591567082480 ) ) ;
#13350=CARTESIAN_POINT ( 'NONE',  ( 5.560781378645573980, 6.809993116116507654E-16, -4.000000000000000000 ) ) ;
#13353=DIRECTION ( 'NONE',  ( 1.000000000000000000, 0.000000000000000000, 0.000000000000000000 ) ) ;
#13360=ORIENTED_EDGE ( 'NONE', *, *, #12182, .T. ) ;
#13381=CARTESIAN_POINT ( 'NONE',  ( -4.000000000000000000, 2.309401076758498483, -3.433295621305379353 ) ) ;
#13395=EDGE_CURVE ( 'NONE', #13559, #2940, #5572, .T. ) ;
#13419=CARTESIAN_POINT ( 'NONE',  ( -4.154094228333736538, -2.398367420967545627, -3.721909803043222276 ) ) ;
#13425=FACE_OUTER_BOUND ( 'NONE', #715, .T. ) ;
#13430=DIRECTION ( 'NONE',  ( 0.000000000000000000, 0.000000000000000000, -1.000000000000000000 ) ) ;
#13433=CARTESIAN_POINT ( 'NONE',  ( -0.1404048886732797152, -4.699864953788083888, -3.686887068327043160 ) ) ;
#13448=VECTOR ( 'NONE', #9429, 1000.000000000000000 ) ;
#13465=ADVANCED_FACE ( 'NONE', ( #15684 ), #7921, .F. ) ;
#13467=ORIENTED_EDGE ( 'NONE', *, *, #6096, .T. ) ;
#13487=ORIENTED_EDGE ( 'NONE', *, *, #6518, .F. ) ;
#13496=AXIS2_PLACEMENT_3D ( 'NONE', #15182, #7824, #7730 ) ;
#13511=CARTESIAN_POINT ( 'NONE',  ( -4.211399284164270895, 2.459729995988205964, -3.751162237960538715 ) ) ;
#13520=FACE_OUTER_BOUND ( 'NONE', #4594, .T. ) ;
#13523=EDGE_LOOP ( 'NONE', ( #6334, #5541, #14855, #352 ) ) ;
#13527=DIRECTION ( 'NONE',  ( -1.000000000000000000, 0.000000000000000000, 0.000000000000000000 ) ) ;
#13559=VERTEX_POINT ( 'NONE', #14978 ) ;
#13560=CARTESIAN_POINT ( 'NONE',  ( 1.567478505476134606E-15, 4.618802153517012066, -3.433295621305382905 ) ) ;
#13565=CARTESIAN_POINT ( 'NONE',  ( 1.317756351988342622, -3.857995168970215438, -0.04852650426602527628 ) ) ;
#13575=ORIENTED_EDGE ( 'NONE', *, *, #5909, .T. ) ;
#13589=ORIENTED_EDGE ( 'NONE', *, *, #6644, .F. ) ;
#13607=DIRECTION ( 'NONE',  ( -1.000000000000000000, 0.000000000000000000, 0.000000000000000000 ) ) ;
#13634=EDGE_CURVE ( 'NONE', #2509, #5072, #9855, .T. ) ;
#13636=AXIS2_PLACEMENT_3D ( 'NONE', #2465, #19037, #4307 ) ;
#13674=EDGE_LOOP ( 'NONE', ( #65, #13487 ) ) ;
#13682=CARTESIAN_POINT ( 'NONE',  ( 2.344047193898588954, 3.265465875126468021, -5.031375706690542042E-16 ) ) ;
#13704=CARTESIAN_POINT ( 'NONE',  ( -4.024497503033519941, -2.323544716729390558, -3.572167766733381544 ) ) ;
#13779=LINE ( 'NONE', #11925, #696 ) ;
#13806=CARTESIAN_POINT ( 'NONE',  ( 1.312671235360372224, 3.860931062424219462, -0.05923475698270440348 ) ) ;
#13864=CARTESIAN_POINT ( 'NONE',  ( 4.211140560182196957, -2.431303136016555122, -3.745885042887436622 ) ) ;
#13868=DIRECTION ( 'NONE',  ( 0.000000000000000000, 0.000000000000000000, -1.000000000000000000 ) ) ;
#13887=B_SPLINE_CURVE_WITH_KNOTS ( 'NONE', 3,
 ( #3185, #9145, #3268, #509 ),
 .UNSPECIFIED., .F., .F.,
 ( 4, 4 ),
 ( 0.000000000000000000, 0.002452478801916361129 ),
 .UNSPECIFIED. ) ;
#13897=CARTESIAN_POINT ( 'NONE',  ( 0.000000000000000000, 0.000000000000000000, -4.000000000000000000 ) ) ;
#13908=CARTESIAN_POINT ( 'NONE',  ( -2.500000000000000444, 3.061616997868383634E-16, -5.000000000000000888 ) ) ;
#13969=ORIENTED_EDGE ( 'NONE', *, *, #7471, .F. ) ;
#13978=AXIS2_PLACEMENT_3D ( 'NONE', #5343, #12795, #6806 ) ;
#13985=CARTESIAN_POINT ( 'NONE',  ( 3.999999999999999112, 1.941961291383486277, -0.3515519931180248192 ) ) ;
#14038=COLOUR_RGB ( '',1.000000000000000000, 0.9490196078431372140, 0.9098039215686274384 ) ;
#14044=ORIENTED_EDGE ( 'NONE', *, *, #11956, .T. ) ;
#14052=CARTESIAN_POINT ( 'NONE',  ( -2.100000000000000089, 2.571758278209441957E-16, -5.000000000000000000 ) ) ;
#14075=SHAPE_REPRESENTATION_RELATIONSHIP ( 'NONE' , 'NONE' ,  #17450, #11045 ) ;
#14110=CARTESIAN_POINT ( 'NONE',  ( 0.000000000000000000, 0.000000000000000000, 0.000000000000000000 ) ) ;
#14124=PRODUCT_DEFINITION_SHAPE ( 'NONE', 'NONE',  #10570 ) ;
#14141=VERTEX_POINT ( 'NONE', #17917 ) ;
#14149=EDGE_LOOP ( 'NONE', ( #5895, #16347, #11399, #14490 ) ) ;
#14153=CARTESIAN_POINT ( 'NONE',  ( -0.6507732100473471171, 4.243078065514775510, -0.2236248678334823436 ) ) ;
#14165=CARTESIAN_POINT ( 'NONE',  ( -5.384454397937118664, 6.594054843588581554E-16, -4.484454397937119197 ) ) ;
#14172=EDGE_CURVE ( 'NONE', #5072, #1514, #15953, .T. ) ;
#14176=ORIENTED_EDGE ( 'NONE', *, *, #13634, .T. ) ;
#14179=ORIENTED_EDGE ( 'NONE', *, *, #17483, .T. ) ;
#14262=CARTESIAN_POINT ( 'NONE',  ( -6.259644161404860030E-16, -4.618802153517027165, -3.433295621305388234 ) ) ;
#14267=ORIENTED_EDGE ( 'NONE', *, *, #18591, .T. ) ;
#14279=CARTESIAN_POINT ( 'NONE',  ( 4.000000000000000000, 0.000000000000000000, 0.000000000000000000 ) ) ;
#14290=ORIENTED_EDGE ( 'NONE', *, *, #10216, .F. ) ;
#14291=CARTESIAN_POINT ( 'NONE',  ( 4.197310751797292738, 0.8178363989516252985, -3.502498386812444409 ) ) ;
#14324=CARTESIAN_POINT ( 'NONE',  ( 4.204015924366189871, -1.626724848190933548, -3.610627190413393084 ) ) ;
#14335=CIRCLE ( 'NONE', #6512, 4.000000000000000000 ) ;
#14354=DIRECTION ( 'NONE',  ( -0.000000000000000000, -0.000000000000000000, 1.000000000000000000 ) ) ;
#14368=FILL_AREA_STYLE ('',( #11038 ) ) ;
#14374=DIRECTION ( 'NONE',  ( 1.000000000000000000, 0.000000000000000000, 0.000000000000000000 ) ) ;
#14394=ORIENTED_EDGE ( 'NONE', *, *, #7011, .T. ) ;
#14396=ADVANCED_FACE ( 'NONE', ( #9927 ), #12586, .T. ) ;
#14420=AXIS2_PLACEMENT_3D ( 'NONE', #15983, #11654, #2573 ) ;
#14424=CARTESIAN_POINT ( 'NONE',  ( 2.059999999999998721, 0.000000000000000000, -0.3080913168122742518 ) ) ;
#14490=ORIENTED_EDGE ( 'NONE', *, *, #13395, .F. ) ;
#14508=CARTESIAN_POINT ( 'NONE',  ( -3.333333333333332149, -2.694301256218264218, -3.300726591567082036 ) ) ;
#14513=CARTESIAN_POINT ( 'NONE',  ( -1.390230914382372118, -4.043987460488664532, -3.502507215260523665 ) ) ;
#14538=CARTESIAN_POINT ( 'NONE',  ( 4.000000000000000000, 2.309401076758497151, -3.433295621305379353 ) ) ;
#14554=CARTESIAN_POINT ( 'NONE',  ( -3.264650091097280831E-13, -4.796980096169642493, -3.721999068284424617 ) ) ;
#14571=CARTESIAN_POINT ( 'NONE',  ( 0.1750025118121568690, 4.719839900820621104, -3.469254087858248070 ) ) ;
#14608=CARTESIAN_POINT ( 'NONE',  ( -1.274258131565027874, -3.883108878240886241, -3.220599429844051009 ) ) ;
#14612=VECTOR ( 'NONE', #9235, 1000.000000000000000 ) ;
#14613=CARTESIAN_POINT ( 'NONE',  ( 1.411581201560190495E-15, 4.862606272033091592, -3.745885042887436622 ) ) ;
#14653=ORIENTED_EDGE ( 'NONE', *, *, #17208, .F. ) ;
#14670=CARTESIAN_POINT ( 'NONE',  ( -4.236525694536558362, 2.416953475386465211, -3.751298745799836354 ) ) ;
#14699=CARTESIAN_POINT ( 'NONE',  ( 4.175648173966055587, -2.207990556236547608, -3.469390959564065291 ) ) ;
#14707=B_SPLINE_CURVE_WITH_KNOTS ( 'NONE', 3,
 ( #14262, #8584, #15653, #2331, #14554, #6628 ),
 .UNSPECIFIED., .F., .F.,
 ( 4, 2, 4 ),
 ( 0.000000000000000000, 0.0002095117440854740156, 0.0004190234881709480313 ),
 .UNSPECIFIED. ) ;
#14711=CARTESIAN_POINT ( 'NONE',  ( -1.287237434361707233, -3.875615274277397937, -3.430618716626816500 ) ) ;
#14729=AXIS2_PLACEMENT_3D ( 'NONE', #495, #15694, #2275 ) ;
#14740=CARTESIAN_POINT ( 'NONE',  ( 0.6507732100473444525, -4.243078065514795050, -0.2236248678334952777 ) ) ;
#14756=CARTESIAN_POINT ( 'NONE',  ( -4.000000000000000000, -2.309401076758515803, -0.4999999999999995559 ) ) ;
#14765=VERTEX_POINT ( 'NONE', #15685 ) ;
#14782=CARTESIAN_POINT ( 'NONE',  ( -1.144235203016679359, -3.958177651039096911, -0.09382832055446428676 ) ) ;
#14804=CARTESIAN_POINT ( 'NONE',  ( -2.000000000000002665, -3.464101615137770374, -3.142992957459237680 ) ) ;
#14825=EDGE_CURVE ( 'NONE', #12888, #7410, #11846, .T. ) ;
#14830=TOROIDAL_SURFACE ( 'NONE', #6695, 5.384454397937118664, 0.5155456020628804703 ) ;
#14854=CARTESIAN_POINT ( 'NONE',  ( -0.6666666666666651864, 4.233901974057260098, -3.300726591567081147 ) ) ;
#14855=ORIENTED_EDGE ( 'NONE', *, *, #10471, .F. ) ;
#14875=FACE_OUTER_BOUND ( 'NONE', #15716, .T. ) ;
#14891=CARTESIAN_POINT ( 'NONE',  ( 1.654252653721905331, 3.663718938583014229, -0.01223254789873410957 ) ) ;
#14900=CARTESIAN_POINT ( 'NONE',  ( 1.243802165048773611, -3.900692638707475624, -3.223146290109810241 ) ) ;
#14939=FACE_OUTER_BOUND ( 'NONE', #8806, .T. ) ;
#14978=CARTESIAN_POINT ( 'NONE',  ( -2.100000000000000089, 2.571758278209441957E-16, -4.694516984716113228 ) ) ;
#15048=AXIS2_PLACEMENT_3D ( 'NONE', #10472, #13527, #2947 ) ;
#15078=ADVANCED_FACE ( 'NONE', ( #13520 ), #17494, .T. ) ;
#15095=CARTESIAN_POINT ( 'NONE',  ( 0.6448876103708359731, 4.246476118072354922, -0.2256878752776725616 ) ) ;
#15096=B_SPLINE_CURVE_WITH_KNOTS ( 'NONE', 3,
 ( #13065, #5615, #1208, #1021, #2786, #8748 ),
 .UNSPECIFIED., .F., .F.,
 ( 4, 2, 4 ),
 ( -3.640115492410698714E-06, 0.0002066546034006521879, 0.0004169493222937151081 ),
 .UNSPECIFIED. ) ;
#15099=CARTESIAN_POINT ( 'NONE',  ( 8.673617379884035472E-16, 4.618802153517012954, -5.000000000000000000 ) ) ;
#15103=CARTESIAN_POINT ( 'NONE',  ( -0.1750025118121544265, -4.719839900820635314, -3.469254087858253399 ) ) ;
#15160=VECTOR ( 'NONE', #18075, 1000.000000000000227 ) ;
#15166=CARTESIAN_POINT ( 'NONE',  ( 4.000000000000000000, -1.942223658245635809, -0.3516579909967643691 ) ) ;
#15182=CARTESIAN_POINT ( 'NONE',  ( 0.000000000000000000, 0.000000000000000000, -25.03750572909317285 ) ) ;
#15192=CARTESIAN_POINT ( 'NONE',  ( -2.500000000000000444, 3.061616997868383634E-16, -25.03750572909317285 ) ) ;
#15234=CARTESIAN_POINT ( 'NONE',  ( 1.393927851585479161, -4.043713361053543842, -3.526374918436840922 ) ) ;
#15255=CARTESIAN_POINT ( 'NONE',  ( 3.999999999999999112, -0.7890432684750902093, -0.04868663549882291247 ) ) ;
#15301=DIRECTION ( 'NONE',  ( -1.000000000000000000, 0.000000000000000000, 0.000000000000000000 ) ) ;
#15326=ORIENTED_EDGE ( 'NONE', *, *, #18277, .T. ) ;
#15341=ORIENTED_EDGE ( 'NONE', *, *, #1707, .T. ) ;
#15352=CARTESIAN_POINT ( 'NONE',  ( 0.000000000000000000, 0.000000000000000000, 0.000000000000000000 ) ) ;
#15396=CARTESIAN_POINT ( 'NONE',  ( -4.000000000000000000, 2.309401076758498483, -3.433295621305379353 ) ) ;
#15450=CARTESIAN_POINT ( 'NONE',  ( 0.000000000000000000, 0.000000000000000000, 0.000000000000000000 ) ) ;
#15464=ORIENTED_EDGE ( 'NONE', *, *, #12263, .T. ) ;
#15494=ADVANCED_FACE ( 'NONE', ( #11816 ), #4184, .F. ) ;
#15520=CARTESIAN_POINT ( 'NONE',  ( 4.211140560182196957, -2.431303136016555122, -3.745885042887436622 ) ) ;
#15527=DIRECTION ( 'NONE',  ( -1.000000000000000000, 0.000000000000000000, 0.000000000000000000 ) ) ;
#15528=ORIENTED_EDGE ( 'NONE', *, *, #1731, .F. ) ;
#15548=DIRECTION ( 'NONE',  ( -0.000000000000000000, -0.000000000000000000, 1.000000000000000000 ) ) ;
#15555=SURFACE_STYLE_USAGE ( .BOTH. , #3698 ) ;
#15570=CARTESIAN_POINT ( 'NONE',  ( 4.000000000000000000, 0.3987449864460005378, -0.01220643443059817035 ) ) ;
#15574=DIRECTION ( 'NONE',  ( -0.000000000000000000, -0.000000000000000000, 1.000000000000000000 ) ) ;
#15577=CIRCLE ( 'NONE', #560, 2.100000000000000089 ) ;
#15591=DIRECTION ( 'NONE',  ( 0.000000000000000000, 0.000000000000000000, -1.000000000000000000 ) ) ;
#15594=CARTESIAN_POINT ( 'NONE',  ( -4.211140560182196957, -2.431303136016552013, -3.745885042887436178 ) ) ;
#15628=ORIENTED_EDGE ( 'NONE', *, *, #16666, .T. ) ;
#15636=ORIENTED_EDGE ( 'NONE', *, *, #9857, .T. ) ;
#15653=CARTESIAN_POINT ( 'NONE',  ( -1.240299975428113101E-15, -4.647091401871173311, -3.572172305156514849 ) ) ;
#15668=VECTOR ( 'NONE', #19113, 1000.000000000000227 ) ;
#15680=AXIS2_PLACEMENT_3D ( 'NONE', #3596, #15548, #4786 ) ;
#15684=FACE_OUTER_BOUND ( 'NONE', #9477, .T. ) ;
#15685=CARTESIAN_POINT ( 'NONE',  ( 4.000000000000000000, -2.309401076758514915, -3.433295621305383349 ) ) ;
#15689=CARTESIAN_POINT ( 'NONE',  ( -3.999999999999999112, 1.539600717838996324, -3.300726591567078039 ) ) ;
#15694=DIRECTION ( 'NONE',  ( 0.000000000000000000, 0.000000000000000000, -1.000000000000000000 ) ) ;
#15695=CARTESIAN_POINT ( 'NONE',  ( 0.1404048886732821022, 4.699864953788070565, -3.686887068327037387 ) ) ;
#15699=CARTESIAN_POINT ( 'NONE',  ( -6.259644161404860030E-16, -4.618802153517027165, -3.433295621305388234 ) ) ;
#15716=EDGE_LOOP ( 'NONE', ( #15636, #18135, #12759, #362, #7503 ) ) ;
#15731=B_SPLINE_CURVE_WITH_KNOTS ( 'NONE', 3,
 ( #15396, #15689, #18557, #2270, #8225 ),
 .UNSPECIFIED., .F., .F.,
 ( 4, 1, 4 ),
 ( 0.000000000000000000, 0.002309401076758505790, 0.004618802153517011580 ),
 .UNSPECIFIED. ) ;
#15779=ORIENTED_EDGE ( 'NONE', *, *, #11164, .F. ) ;
#15789=AXIS2_PLACEMENT_3D ( 'NONE', #18480, #517, #16808 ) ;
#15803=EDGE_LOOP ( 'NONE', ( #12684, #907, #8272, #7985 ) ) ;
#15883=EDGE_CURVE ( 'NONE', #8263, #18115, #2623, .T. ) ;
#15899=CARTESIAN_POINT ( 'NONE',  ( 1.567478505476134606E-15, 4.618802153517012066, -3.433295621305382905 ) ) ;
#15941=CARTESIAN_POINT ( 'NONE',  ( -4.000000000000000000, -2.309401076758512694, -5.000000000000000000 ) ) ;
#15953=B_SPLINE_CURVE_WITH_KNOTS ( 'NONE', 3,
 ( #16053, #8875, #8588, #16439, #8780, #14756 ),
 .UNSPECIFIED., .F., .F.,
 ( 4, 2, 4 ),
 ( 0.002365888236228001588, 0.003551327329835089319, 0.004736766423442177049 ),
 .UNSPECIFIED. ) ;
#15959=CYLINDRICAL_SURFACE ( 'NONE', #2402, 2.100000000000000089 ) ;
#15983=CARTESIAN_POINT ( 'NONE',  ( 0.000000000000000000, 0.000000000000000000, -4.974599999999998801 ) ) ;
#16006=CARTESIAN_POINT ( 'NONE',  ( 0.02511973781850649831, -4.877415612947427981, -3.751298745799844792 ) ) ;
#16022=B_SPLINE_CURVE_WITH_KNOTS ( 'NONE', 3,
 ( #2688, #12767, #2393, #14324, #16108, #906 ),
 .UNSPECIFIED., .F., .F.,
 ( 4, 2, 4 ),
 ( 0.002452478801916361129, 0.003676905084148001344, 0.004901331366379641126 ),
 .UNSPECIFIED. ) ;
#16028=ORIENTED_EDGE ( 'NONE', *, *, #1273, .T. ) ;
#16048=CARTESIAN_POINT ( 'NONE',  ( 1.391697335622810172, 4.043246145443375461, -3.503898532754365913 ) ) ;
#16053=CARTESIAN_POINT ( 'NONE',  ( -2.000000000000007550, -3.464101615137749945, 0.000000000000000000 ) ) ;
#16101=CARTESIAN_POINT ( 'NONE',  ( -4.175002511812151873, -2.208363329454905877, -3.469254087858246738 ) ) ;
#16108=CARTESIAN_POINT ( 'NONE',  ( 4.207491450040567571, -2.029819825146485179, -3.671670828759567407 ) ) ;
#16114=EDGE_CURVE ( 'NONE', #5403, #18909, #11565, .T. ) ;
#16118=CARTESIAN_POINT ( 'NONE',  ( 0.000000000000000000, 0.000000000000000000, 0.000000000000000000 ) ) ;
#16127=ORIENTED_EDGE ( 'NONE', *, *, #8421, .T. ) ;
#16132=EDGE_CURVE ( 'NONE', #10976, #71, #16800, .T. ) ;
#16166=EDGE_CURVE ( 'NONE', #10751, #11229, #13887, .T. ) ;
#16188=CARTESIAN_POINT ( 'NONE',  ( -4.000000000000000000, -2.309401076758512694, -3.433295621305382461 ) ) ;
#16191=DIRECTION ( 'NONE',  ( 1.000000000000000000, 0.000000000000000000, 0.000000000000000000 ) ) ;
#16194=CARTESIAN_POINT ( 'NONE',  ( -0.5449313310646672903, -4.304185902836978883, -3.316620875263469159 ) ) ;
#16198=CARTESIAN_POINT ( 'NONE',  ( -2.805705207896067144, 3.226868319750155312, -3.503898532754364581 ) ) ;
#16205=CARTESIAN_POINT ( 'NONE',  ( -0.1756481739660520902, 4.720212674038980261, -3.469390959564065291 ) ) ;
#16217=AXIS2_PLACEMENT_3D ( 'NONE', #5149, #840, #12699 ) ;
#16247=ORIENTED_EDGE ( 'NONE', *, *, #7302, .T. ) ;
#16267=ORIENTED_EDGE ( 'NONE', *, *, #5778, .T. ) ;
#16347=ORIENTED_EDGE ( 'NONE', *, *, #1731, .T. ) ;
#16352=EDGE_CURVE ( 'NONE', #71, #9774, #8444, .T. ) ;
#16353=CONICAL_SURFACE ( 'NONE', #6012, 2.059999999999998721, 0.9599310885968738161 ) ;
#16379=ORIENTED_EDGE ( 'NONE', *, *, #14825, .T. ) ;
#16382=CARTESIAN_POINT ( 'NONE',  ( 2.000000000000008882, 3.464101615137749945, 0.000000000000000000 ) ) ;
#16393=CARTESIAN_POINT ( 'NONE',  ( -4.207491450040567571, 2.029819825146470524, -3.671670828759566074 ) ) ;
#16418=ORIENTED_EDGE ( 'NONE', *, *, #8064, .T. ) ;
#16439=CARTESIAN_POINT ( 'NONE',  ( -3.349226789952655547, -2.685125164760744809, -0.2236248678334863682 ) ) ;
#16484=CARTESIAN_POINT ( 'NONE',  ( 3.436319922986518449, -2.634841920959471562, -3.531542292954761741 ) ) ;
#16492=SHAPE_DEFINITION_REPRESENTATION ( #14124, #17450 ) ;
#16521=CARTESIAN_POINT ( 'NONE',  ( 2.500000000000000444, 0.000000000000000000, -25.03750572909317285 ) ) ;
#16572=PLANE ( 'NONE',  #15048 ) ;
#16614=CARTESIAN_POINT ( 'NONE',  ( 2.290893957444128645E-15, 4.647089433458768681, -3.572167766733382877 ) ) ;
#16637=ORIENTED_EDGE ( 'NONE', *, *, #10774, .F. ) ;
#16652=DIRECTION ( 'NONE',  ( 0.000000000000000000, 0.000000000000000000, 1.000000000000000000 ) ) ;
#16666=EDGE_CURVE ( 'NONE', #12888, #14141, #1579, .T. ) ;
#16679=AXIS2_PLACEMENT_3D ( 'NONE', #1500, #12173, #13353 ) ;
#16681=DIRECTION ( 'NONE',  ( -1.000000000000000000, 0.000000000000000000, 0.000000000000000000 ) ) ;
#16717=B_SPLINE_CURVE_WITH_KNOTS ( 'NONE', 3,
 ( #363, #5239, #9744, #14153, #12400, #9355 ),
 .UNSPECIFIED., .F., .F.,
 ( 4, 2, 4 ),
 ( 0.002365888236227977302, 0.003551327329835078910, 0.004736766423442180518 ),
 .UNSPECIFIED. ) ;
#16729=ORIENTED_EDGE ( 'NONE', *, *, #7013, .F. ) ;
#16738=DIRECTION ( 'NONE',  ( 1.000000000000000000, 0.000000000000000000, 0.000000000000000000 ) ) ;
#16762=CARTESIAN_POINT ( 'NONE',  ( 0.3198814748697593746, 4.434118497892183264, -0.3507732604232499107 ) ) ;
#16788=CARTESIAN_POINT ( 'NONE',  ( 2.500000000000000888, 3.061616997868384127E-16, -4.974599999999998801 ) ) ;
#16800=LINE ( 'NONE', #6207, #13448 ) ;
#16802=B_SPLINE_CURVE_WITH_KNOTS ( 'NONE', 3,
 ( #3284, #3570, #9246, #4764 ),
 .UNSPECIFIED., .F., .F.,
 ( 4, 4 ),
 ( 0.000000000000000000, 0.002452478801916376308 ),
 .UNSPECIFIED. ) ;
#16808=DIRECTION ( 'NONE',  ( 0.8660254037844374864, -0.5000000000000018874, 0.000000000000000000 ) ) ;
#16812=( BOUNDED_SURFACE ( )  B_SPLINE_SURFACE ( 3, 2, ( 
 ( #3953, #9914, #10115 ),
 ( #4052, #10014, #2500 ),
 ( #2691, #8454, #13158 ),
 ( #10201, #17685, #1017 ),
 ( #6979, #12959, #19174 ),
 ( #16205, #1308, #7567 ) ),
 .UNSPECIFIED., .F., .F., .F. ) 
 B_SPLINE_SURFACE_WITH_KNOTS ( ( 4, 2, 4 ),
 ( 3, 3 ),
 ( 0.02032853247518126225, 0.02278863295364821212, 0.02524873343211516200 ),
 ( 0.000000000000000000, 1.000000000000000000 ),
 .UNSPECIFIED. ) 
 GEOMETRIC_REPRESENTATION_ITEM ( )  RATIONAL_B_SPLINE_SURFACE ( (
 ( 1.000000000000000000, 0.8047781615896835161, 1.000000000000000000),
 ( 1.000000000000000000, 0.8123767586291043008, 1.000000000000000000),
 ( 1.000000000000000000, 0.8190662415562011134, 1.000000000000000000),
 ( 1.000000000000000000, 0.8192361015671398849, 1.000000000000000000),
 ( 1.000000000000000000, 0.8126135807102121689, 1.000000000000000000),
 ( 1.000000000000000000, 0.8047712338318585568, 1.000000000000000000) ) ) 
 REPRESENTATION_ITEM ( '' )  SURFACE ( )  );
#16847=VERTEX_POINT ( 'NONE', #13908 ) ;
#16861=DIRECTION ( 'NONE',  ( 0.000000000000000000, 0.000000000000000000, -1.000000000000000000 ) ) ;
#16922=VERTEX_POINT ( 'NONE', #9072 ) ;
#16924=CIRCLE ( 'NONE', #10651, 0.5155456020628804703 ) ;
#16937=VECTOR ( 'NONE', #15574, 1000.000000000000000 ) ;
#16953=CIRCLE ( 'NONE', #973, 2.500000000000000444 ) ;
#16980=B_SPLINE_CURVE_WITH_KNOTS ( 'NONE', 3,
 ( #3662, #8161, #7967, #2302, #11007, #11294, #12120, #7620 ),
 .UNSPECIFIED., .F., .F.,
 ( 4, 2, 2, 4 ),
 ( 2.465131517071352357E-07, 0.001183067374689843057, 0.001774477805458910071, 0.002365888236227977302 ),
 .UNSPECIFIED. ) ;
#17010=B_SPLINE_CURVE_WITH_KNOTS ( 'NONE', 3,
 ( #17173, #3636, #499, #2174, #4913, #10786, #12356, #15594 ),
 .UNSPECIFIED., .F., .F.,
 ( 4, 2, 2, 4 ),
 ( 0.000000000000000000, 0.002450665683189818828, 0.003675998524784728459, 0.004901331366379638524 ),
 .UNSPECIFIED. ) ;
#17043=( NAMED_UNIT ( * ) SI_UNIT ( $, .STERADIAN. ) SOLID_ANGLE_UNIT ( ) );
#17057=CARTESIAN_POINT ( 'NONE',  ( 4.000000000000000000, 2.309401076758515803, -0.4999999999999995559 ) ) ;
#17066=ORIENTED_EDGE ( 'NONE', *, *, #6636, .T. ) ;
#17086=ADVANCED_FACE ( 'NONE', ( #2169 ), #17553, .T. ) ;
#17115=CARTESIAN_POINT ( 'NONE',  ( -4.000000000000000000, 2.309401076758498483, -0.4999999999999927280 ) ) ;
#17132=CARTESIAN_POINT ( 'NONE',  ( 3.510273485745307731, 2.827716139362654424, -3.610536846335885564 ) ) ;
#17163=ORIENTED_EDGE ( 'NONE', *, *, #11567, .T. ) ;
#17170=CARTESIAN_POINT ( 'NONE',  ( -4.175648173966055587, 2.207990556236529844, -3.469390959564062626 ) ) ;
#17173=CARTESIAN_POINT ( 'NONE',  ( -6.473970235329672780E-16, -4.862606272033106691, -3.745885042887442395 ) ) ;
#17208=EDGE_CURVE ( 'NONE', #71, #1748, #17569, .T. ) ;
#17238=ADVANCED_FACE ( 'NONE', ( #12447 ), #5346, .T. ) ;
#17244=B_SPLINE_CURVE_WITH_KNOTS ( 'NONE', 3,
 ( #5877, #13419, #11843, #13704, #4702, #6256 ),
 .UNSPECIFIED., .F., .F.,
 ( 4, 2, 4 ),
 ( -3.640115492409406142E-06, 0.0002066546034006526487, 0.0004169493222937146744 ),
 .UNSPECIFIED. ) ;
#17251=CARTESIAN_POINT ( 'NONE',  ( 4.000000000000000000, 0.9868501483902631932, -0.09357334158579604100 ) ) ;
#17264=CARTESIAN_POINT ( 'NONE',  ( 4.000000000000000888, -0.8578082829538523635, -3.433262215449808696 ) ) ;
#17269=DIRECTION ( 'NONE',  ( 0.000000000000000000, 0.000000000000000000, 1.000000000000000000 ) ) ;
#17299=LINE ( 'NONE', #5412, #11503 ) ;
#17327=DIRECTION ( 'NONE',  ( 0.000000000000000000, 0.000000000000000000, -1.000000000000000000 ) ) ;
#17358=CARTESIAN_POINT ( 'NONE',  ( 4.000000000001088907, 1.658577278524410170, -3.531553309554541720 ) ) ;
#17393=FACE_OUTER_BOUND ( 'NONE', #10078, .T. ) ;
#17444=CARTESIAN_POINT ( 'NONE',  ( 4.000000000000000000, 0.1981133338132474442, 2.382280164152719704E-17 ) ) ;
#17450=SHAPE_REPRESENTATION ( 'hex flange nut gradea_iso_ISO - 4161 - M5 - N', ( #10359 ), #11543 ) ;
#17481=CARTESIAN_POINT ( 'NONE',  ( -0.6810597143197697489, -4.461075778259609770, -3.598441714920717516 ) ) ;
#17483=EDGE_CURVE ( 'NONE', #2940, #5141, #18507, .T. ) ;
#17494=CONICAL_SURFACE ( 'NONE', #9640, 4.000000000000000000, 0.8911886515913786111 ) ;
#17505=CARTESIAN_POINT ( 'NONE',  ( -4.000000000000000888, 1.563622288139195238, -0.2253451193528307472 ) ) ;
#17507=CARTESIAN_POINT ( 'NONE',  ( 4.154306624731137099, 2.398490048084935822, -3.721999068284414847 ) ) ;
#17508=AXIS2_PLACEMENT_3D ( 'NONE', #1244, #5949, #3011 ) ;
#17533=EDGE_LOOP ( 'NONE', ( #8006, #4558, #18716, #2256 ) ) ;
#17540=CARTESIAN_POINT ( 'NONE',  ( -0.6640947660597427138, 4.471078309994878985, -3.602146406945963442 ) ) ;
#17542=CYLINDRICAL_SURFACE ( 'NONE', #19036, 2.500000000000000444 ) ;
#17549=ADVANCED_FACE ( 'NONE', ( #13425 ), #7541, .F. ) ;
#17551=ORIENTED_EDGE ( 'NONE', *, *, #11956, .F. ) ;
#17553=CONICAL_SURFACE ( 'NONE', #2205, 5.560781378645573980, 1.221730476396046816 ) ;
#17554=ADVANCED_FACE ( 'NONE', ( #12048 ), #16572, .F. ) ;
#17561=EDGE_CURVE ( 'NONE', #4790, #7410, #18616, .T. ) ;
#17569=CIRCLE ( 'NONE', #14729, 2.100000000000000089 ) ;
#17571=EDGE_CURVE ( 'NONE', #1014, #7410, #18204, .T. ) ;
#17643=CARTESIAN_POINT ( 'NONE',  ( -3.455068668934486276, 2.624017327439035707, -3.316620875263955437 ) ) ;
#17655=CARTESIAN_POINT ( 'NONE',  ( 0.000000000000000000, 0.000000000000000000, -4.694516984716113228 ) ) ;
#17666=CARTESIAN_POINT ( 'NONE',  ( -0.6666666666666666297, -4.233901974057276973, -3.300726591567087365 ) ) ;
#17685=CARTESIAN_POINT ( 'NONE',  ( 1.287237434362044075, 3.875615274277557809, -3.430618716626812059 ) ) ;
#17723=EDGE_LOOP ( 'NONE', ( #1369, #14267, #13360, #4547, #17163 ) ) ;
#17734=CARTESIAN_POINT ( 'NONE',  ( -4.000000000000000000, 0.000000000000000000, 0.000000000000000000 ) ) ;
#17737=DIRECTION ( 'NONE',  ( 1.000000000000000000, 0.000000000000000000, 0.000000000000000000 ) ) ;
#17837=CARTESIAN_POINT ( 'NONE',  ( -4.000000000000000000, -0.8382240730041925492, -3.220610619767135141 ) ) ;
#17842=CARTESIAN_POINT ( 'NONE',  ( -1.654252653721913102, -3.663718938583024443, -0.01223254789874440342 ) ) ;
#17866=CARTESIAN_POINT ( 'NONE',  ( -4.211140560182196957, 2.431303136016537803, -3.745885042887433514 ) ) ;
#17917=CARTESIAN_POINT ( 'NONE',  ( 2.000000000000005329, -3.464101615137751722, 0.000000000000000000 ) ) ;
#17927=EDGE_CURVE ( 'NONE', #5450, #5403, #5967, .T. ) ;
#17941=CARTESIAN_POINT ( 'NONE',  ( -4.000000000000000000, -0.8232339106130515116, -3.430630286862743183 ) ) ;
#17946=CARTESIAN_POINT ( 'NONE',  ( -0.3198814748697807464, -4.434118497892185040, -0.3507732604232532969 ) ) ;
#17958=CARTESIAN_POINT ( 'NONE',  ( 2.682243648011666703, 3.070208061305304881, -0.04852650426601266831 ) ) ;
#17963=CARTESIAN_POINT ( 'NONE',  ( 1.257172072275274388, -3.892973519170983110, -3.433252694550781303 ) ) ;
#17972=PRODUCT_CONTEXT ( 'NONE', #18817, 'mechanical' ) ;
#18058=CARTESIAN_POINT ( 'NONE',  ( -4.000000000000000000, -2.309401076758515803, -0.4999999999999995559 ) ) ;
#18075=DIRECTION ( 'NONE',  ( 0.9396926207859138680, 1.150791560227856926E-16, -0.3420201433256536139 ) ) ;
#18115=VERTEX_POINT ( 'NONE', #10392 ) ;
#18130=B_SPLINE_CURVE_WITH_KNOTS ( 'NONE', 3,
 ( #18058, #9559, #7646, #6181, #3692, #12152 ),
 .UNSPECIFIED., .F., .F.,
 ( 4, 2, 4 ),
 ( 0.003358874760055550156, 0.004541967308452096383, 0.005725059856848641743 ),
 .UNSPECIFIED. ) ;
#18135=ORIENTED_EDGE ( 'NONE', *, *, #9498, .F. ) ;
#18145=EDGE_CURVE ( 'NONE', #6664, #8664, #6884, .T. ) ;
#18192=VECTOR ( 'NONE', #13201, 999.9999999999998863 ) ;
#18204=CIRCLE ( 'NONE', #8163, 4.000000000000000000 ) ;
#18222=DIRECTION ( 'NONE',  ( -0.000000000000000000, -0.000000000000000000, 1.000000000000000000 ) ) ;
#18277=EDGE_CURVE ( 'NONE', #1514, #8263, #18130, .T. ) ;
#18291=CARTESIAN_POINT ( 'NONE',  ( 4.000000000000000000, -2.309401076758514915, -3.433295621305383349 ) ) ;
#18315=CARTESIAN_POINT ( 'NONE',  ( 4.000000000000000000, 2.309401076758515803, -0.4999999999999995559 ) ) ;
#18395=EDGE_CURVE ( 'NONE', #442, #7928, #16924, .T. ) ;
#18440=DIRECTION ( 'NONE',  ( -0.000000000000000000, -0.000000000000000000, 1.000000000000000000 ) ) ;
#18480=CARTESIAN_POINT ( 'NONE',  ( -4.000000000000000000, -2.309401076758512694, -5.000000000000000000 ) ) ;
#18481=B_SPLINE_CURVE_WITH_KNOTS ( 'NONE', 3,
 ( #18519, #5061, #16048, #10050, #3982, #17132, #9759, #9655 ),
 .UNSPECIFIED., .F., .F.,
 ( 4, 2, 2, 4 ),
 ( 7.780516681398759253E-20, 0.002450665683189819696, 0.003675998524784729327, 0.004901331366379639391 ),
 .UNSPECIFIED. ) ;
#18507=CIRCLE ( 'NONE', #14420, 2.500000000000000888 ) ;
#18519=CARTESIAN_POINT ( 'NONE',  ( 1.411581201560190495E-15, 4.862606272033091592, -3.745885042887436622 ) ) ;
#18546=LINE ( 'NONE', #15192, #16937 ) ;
#18557=CARTESIAN_POINT ( 'NONE',  ( -4.000000000000000000, -7.806255641895631925E-15, -3.142992957459232350 ) ) ;
#18588=CARTESIAN_POINT ( 'NONE',  ( 5.384454397937118664, 0.000000000000000000, -5.000000000000000000 ) ) ;
#18591=EDGE_CURVE ( 'NONE', #18909, #10423, #3387, .T. ) ;
#18595=EDGE_LOOP ( 'NONE', ( #8525, #986, #377, #13096 ) ) ;
#18599=ORIENTED_EDGE ( 'NONE', *, *, #14172, .F. ) ;
#18602=EDGE_LOOP ( 'NONE', ( #7047, #5685, #3384, #7625, #14044 ) ) ;
#18609=PLANE ( 'NONE',  #16217 ) ;
#18616=B_SPLINE_CURVE_WITH_KNOTS ( 'NONE', 3,
 ( #10380, #16762, #15095, #8909, #13806, #14891, #389, #16382 ),
 .UNSPECIFIED., .F., .F.,
 ( 4, 2, 2, 4 ),
 ( 2.465131517075058656E-07, 0.001183067374689851080, 0.001774477805458923299, 0.002365888236227995517 ),
 .UNSPECIFIED. ) ;
#18619=CONICAL_SURFACE ( 'NONE', #1700, 4.000000000000000000, 0.8911886515913786111 ) ;
#18631=CARTESIAN_POINT ( 'NONE',  ( 1.734723475976807094E-15, 4.618802153517012954, -0.4999999999999995559 ) ) ;
#18643=CARTESIAN_POINT ( 'NONE',  ( 0.000000000000000000, 0.000000000000000000, 0.000000000000000000 ) ) ;
#18685=EDGE_LOOP ( 'NONE', ( #11330, #8818, #18758, #10527, #11382 ) ) ;
#18716=ORIENTED_EDGE ( 'NONE', *, *, #6518, .T. ) ;
#18732=CARTESIAN_POINT ( 'NONE',  ( 4.000000000000000000, -1.677850389431204459, -3.535268758346977513 ) ) ;
#18758=ORIENTED_EDGE ( 'NONE', *, *, #5574, .T. ) ;
#18761=ADVANCED_FACE ( 'NONE', ( #10724 ), #6602, .T. ) ;
#18817=APPLICATION_CONTEXT ( 'automotive_design' ) ;
#18839=CARTESIAN_POINT ( 'NONE',  ( 4.000000000000000000, 1.680228229147133767, -3.316631783032546021 ) ) ;
#18849=AXIS2_PLACEMENT_3D ( 'NONE', #10737, #18222, #16738 ) ;
#18891=ORIENTED_EDGE ( 'NONE', *, *, #5329, .T. ) ;
#18900=CARTESIAN_POINT ( 'NONE',  ( -4.211140560182196957, -2.431303136016552013, -3.745885042887436178 ) ) ;
#18909=VERTEX_POINT ( 'NONE', #15899 ) ;
#18981=CARTESIAN_POINT ( 'NONE',  ( -4.000000000000000000, 0.7924765000094600165, -0.05906175389889745803 ) ) ;
#18984=EDGE_CURVE ( 'NONE', #14141, #5072, #8154, .T. ) ;
#19036=AXIS2_PLACEMENT_3D ( 'NONE', #13015, #11728, #2741 ) ;
#19037=DIRECTION ( 'NONE',  ( 0.000000000000000000, 0.000000000000000000, -1.000000000000000000 ) ) ;
#19056=B_SPLINE_CURVE_WITH_KNOTS ( 'NONE', 3,
 ( #14279, #17444, #15570, #8214, #17251, #5271, #13985, #17057 ),
 .UNSPECIFIED., .F., .F.,
 ( 4, 2, 2, 4 ),
 ( 0.005725059856848645212, 0.006314084072593634418, 0.006903108288338624492, 0.008081156719828603771 ),
 .UNSPECIFIED. ) ;
#19113=DIRECTION ( 'NONE',  ( -0.9396926207859138680, 0.000000000000000000, -0.3420201433256536139 ) ) ;
#19121=EDGE_CURVE ( 'NONE', #9774, #12905, #12544, .T. ) ;
#19144=PRODUCT_DEFINITION_CONTEXT ( 'detailed design', #12034, 'design' ) ;
#19174=CARTESIAN_POINT ( 'NONE',  ( 0.6810597143197052450, 4.461075778259290914, -3.598441714920602053 ) ) ;
#19213=VERTEX_POINT ( 'NONE', #4743 ) ;
#19227=CARTESIAN_POINT ( 'NONE',  ( -4.000000000000000000, -2.512220745329312610, -3.469390707569719901 ) ) ;
#19287=AXIS2_PLACEMENT_3D ( 'NONE', #7616, #1181, #7156 ) ;
#19317=CARTESIAN_POINT ( 'NONE',  ( -3.522875095019672109, 2.820352903225427532, -3.598441714920591394 ) ) ;
#19324=CARTESIAN_POINT ( 'NONE',  ( -4.000000000000000000, 1.677772373332757194, -3.535253723897187506 ) ) ;
#19346=CARTESIAN_POINT ( 'NONE',  ( 2.725741868436127202, -3.045094352033990148, -3.220599429844051453 ) ) ;
#19359=CARTESIAN_POINT ( 'NONE',  ( -4.140404888673278272, -2.228338276487456415, -3.686887068327035166 ) ) ;
#19371=CARTESIAN_POINT ( 'NONE',  ( 4.000000000000000000, 2.309401076758497151, -3.433295621305379353 ) ) ;
#19375=VECTOR ( 'NONE', #319, 1000.000000000000114 ) ;
#19469=COLOUR_RGB('Black',0.12,0.14,0.17);
#19470=FILL_AREA_STYLE_COLOUR('',#19469);
#19471=FILL_AREA_STYLE('',(#19470));
#19472=SURFACE_STYLE_FILL_AREA(#19471);
#19473=SURFACE_SIDE_STYLE('',(#19472));
#19474=SURFACE_STYLE_USAGE(.BOTH.,#19473);
#19475=PRESENTATION_STYLE_ASSIGNMENT((#19474));
ENDSEC;
END-ISO-10303-21;
